ISO-10303-21;
HEADER;
/* Generated by software containing ST-Developer
 * from STEP Tools, Inc. (www.steptools.com) 
 */

FILE_DESCRIPTION(
/* description */ ('CAx-IF Rec.Pracs.---Representation and Presentation of Product Manufa
cturing Information (PMI)---4.0---2014-10-13'),
/* implementation_level */ '2;1');

FILE_NAME(
/* name */ 'Socket Screw 6.step',
/* time_stamp */ '2026-10-24T18:52:33-07:00',
/* author */ (''),
/* organization */ (''),
/* preprocessor_version */ 'ST-DEVELOPER v20.2',
/* originating_system */ 'Autodesk Translation Framework v15.17.0.0',
/* authorisation */ '');

FILE_SCHEMA (('AP242_MANAGED_MODEL_BASED_3D_ENGINEERING_MIM_LF { 1 0 10303 442 2 1 4 }'));
ENDSEC;

DATA;
#10=MECHANICAL_DESIGN_GEOMETRIC_PRESENTATION_REPRESENTATION('',(#440),#34876);
#374=SHAPE_REPRESENTATION_RELATIONSHIP('SRR','None',#35011,#407);
#407=ADVANCED_BREP_SHAPE_REPRESENTATION('',(#473),#34869);
#440=STYLED_ITEM('',(#35161),#473);
#473=MANIFOLD_SOLID_BREP('Socket Screw 6',#19580);
#572=FACE_BOUND('',#6831,.T.);
#573=FACE_BOUND('',#6832,.T.);
#574=FACE_BOUND('',#6833,.T.);
#575=FACE_BOUND('',#6834,.T.);
#576=FACE_BOUND('',#6835,.T.);
#577=FACE_BOUND('',#6836,.T.);
#578=FACE_BOUND('',#6858,.T.);
#579=FACE_BOUND('',#6859,.T.);
#580=FACE_BOUND('',#6860,.T.);
#581=FACE_BOUND('',#6861,.T.);
#582=FACE_BOUND('',#6862,.T.);
#583=FACE_BOUND('',#6863,.T.);
#979=PLANE('',#21905);
#980=PLANE('',#21906);
#981=PLANE('',#21907);
#982=PLANE('',#21908);
#983=PLANE('',#21909);
#984=PLANE('',#21910);
#985=PLANE('',#21911);
#986=PLANE('',#21912);
#987=PLANE('',#21913);
#988=PLANE('',#21914);
#989=PLANE('',#21915);
#990=PLANE('',#21916);
#991=PLANE('',#21917);
#992=PLANE('',#21918);
#993=PLANE('',#21919);
#994=PLANE('',#21920);
#995=PLANE('',#21921);
#996=PLANE('',#21922);
#997=PLANE('',#21923);
#998=PLANE('',#21924);
#999=PLANE('',#21925);
#1000=PLANE('',#21926);
#1001=PLANE('',#21927);
#1002=PLANE('',#21928);
#1003=PLANE('',#21929);
#1004=PLANE('',#21930);
#1005=PLANE('',#21931);
#1006=PLANE('',#21932);
#1007=PLANE('',#21933);
#1008=PLANE('',#21934);
#1009=PLANE('',#21935);
#1010=PLANE('',#21936);
#1011=PLANE('',#21937);
#1012=PLANE('',#21938);
#1013=PLANE('',#21939);
#1014=PLANE('',#21940);
#1015=PLANE('',#21941);
#1016=PLANE('',#21942);
#1017=PLANE('',#21943);
#1018=PLANE('',#21944);
#1019=PLANE('',#21945);
#1020=PLANE('',#21946);
#1021=PLANE('',#21947);
#1022=PLANE('',#21948);
#1023=PLANE('',#21949);
#1024=PLANE('',#21950);
#1025=PLANE('',#21951);
#1026=PLANE('',#21952);
#1027=PLANE('',#21953);
#1028=PLANE('',#21954);
#1029=PLANE('',#21955);
#1030=PLANE('',#21956);
#1031=PLANE('',#21957);
#1032=PLANE('',#21958);
#2363=LINE('',#33590,#3962);
#2364=LINE('',#33592,#3963);
#2365=LINE('',#33594,#3964);
#2366=LINE('',#33595,#3965);
#2367=LINE('',#33598,#3966);
#2368=LINE('',#33600,#3967);
#2369=LINE('',#33601,#3968);
#2370=LINE('',#33604,#3969);
#2371=LINE('',#33606,#3970);
#2372=LINE('',#33607,#3971);
#2373=LINE('',#33609,#3972);
#2374=LINE('',#33610,#3973);
#2375=LINE('',#33614,#3974);
#2376=LINE('',#33616,#3975);
#2377=LINE('',#33618,#3976);
#2378=LINE('',#33619,#3977);
#2379=LINE('',#33622,#3978);
#2380=LINE('',#33624,#3979);
#2381=LINE('',#33625,#3980);
#2382=LINE('',#33628,#3981);
#2383=LINE('',#33630,#3982);
#2384=LINE('',#33631,#3983);
#2385=LINE('',#33633,#3984);
#2386=LINE('',#33634,#3985);
#2387=LINE('',#33638,#3986);
#2388=LINE('',#33640,#3987);
#2389=LINE('',#33642,#3988);
#2390=LINE('',#33643,#3989);
#2391=LINE('',#33646,#3990);
#2392=LINE('',#33648,#3991);
#2393=LINE('',#33649,#3992);
#2394=LINE('',#33652,#3993);
#2395=LINE('',#33654,#3994);
#2396=LINE('',#33655,#3995);
#2397=LINE('',#33657,#3996);
#2398=LINE('',#33658,#3997);
#2399=LINE('',#33662,#3998);
#2400=LINE('',#33664,#3999);
#2401=LINE('',#33666,#4000);
#2402=LINE('',#33667,#4001);
#2403=LINE('',#33670,#4002);
#2404=LINE('',#33672,#4003);
#2405=LINE('',#33673,#4004);
#2406=LINE('',#33676,#4005);
#2407=LINE('',#33678,#4006);
#2408=LINE('',#33679,#4007);
#2409=LINE('',#33681,#4008);
#2410=LINE('',#33682,#4009);
#2411=LINE('',#33686,#4010);
#2412=LINE('',#33688,#4011);
#2413=LINE('',#33690,#4012);
#2414=LINE('',#33691,#4013);
#2415=LINE('',#33694,#4014);
#2416=LINE('',#33696,#4015);
#2417=LINE('',#33697,#4016);
#2418=LINE('',#33700,#4017);
#2419=LINE('',#33702,#4018);
#2420=LINE('',#33703,#4019);
#2421=LINE('',#33705,#4020);
#2422=LINE('',#33706,#4021);
#2423=LINE('',#33710,#4022);
#2424=LINE('',#33712,#4023);
#2425=LINE('',#33714,#4024);
#2426=LINE('',#33715,#4025);
#2427=LINE('',#33718,#4026);
#2428=LINE('',#33720,#4027);
#2429=LINE('',#33721,#4028);
#2430=LINE('',#33724,#4029);
#2431=LINE('',#33726,#4030);
#2432=LINE('',#33727,#4031);
#2433=LINE('',#33729,#4032);
#2434=LINE('',#33730,#4033);
#2435=LINE('',#33734,#4034);
#2436=LINE('',#33736,#4035);
#2437=LINE('',#33738,#4036);
#2438=LINE('',#33739,#4037);
#2439=LINE('',#33742,#4038);
#2440=LINE('',#33744,#4039);
#2441=LINE('',#33745,#4040);
#2442=LINE('',#33748,#4041);
#2443=LINE('',#33750,#4042);
#2444=LINE('',#33751,#4043);
#2445=LINE('',#33754,#4044);
#2446=LINE('',#33756,#4045);
#2447=LINE('',#33758,#4046);
#2448=LINE('',#33760,#4047);
#2449=LINE('',#33761,#4048);
#2450=LINE('',#33764,#4049);
#2451=LINE('',#33766,#4050);
#2452=LINE('',#33768,#4051);
#2453=LINE('',#33769,#4052);
#2454=LINE('',#33772,#4053);
#2455=LINE('',#33774,#4054);
#2456=LINE('',#33775,#4055);
#2457=LINE('',#33778,#4056);
#2458=LINE('',#33780,#4057);
#2459=LINE('',#33782,#4058);
#2460=LINE('',#33784,#4059);
#2461=LINE('',#33786,#4060);
#2462=LINE('',#33788,#4061);
#2463=LINE('',#33790,#4062);
#2464=LINE('',#33792,#4063);
#2465=LINE('',#33794,#4064);
#2466=LINE('',#33795,#4065);
#2467=LINE('',#33799,#4066);
#2468=LINE('',#33800,#4067);
#2469=LINE('',#33801,#4068);
#2470=LINE('',#33805,#4069);
#2471=LINE('',#33807,#4070);
#2472=LINE('',#33809,#4071);
#2473=LINE('',#33810,#4072);
#2474=LINE('',#33812,#4073);
#2475=LINE('',#33813,#4074);
#2476=LINE('',#33816,#4075);
#2477=LINE('',#33818,#4076);
#2478=LINE('',#33820,#4077);
#2479=LINE('',#33821,#4078);
#2480=LINE('',#33823,#4079);
#2481=LINE('',#33825,#4080);
#2482=LINE('',#33827,#4081);
#2483=LINE('',#33828,#4082);
#2484=LINE('',#33830,#4083);
#2485=LINE('',#33832,#4084);
#2486=LINE('',#33834,#4085);
#2487=LINE('',#33836,#4086);
#2488=LINE('',#33837,#4087);
#2489=LINE('',#33841,#4088);
#2490=LINE('',#33842,#4089);
#2491=LINE('',#33843,#4090);
#2492=LINE('',#33846,#4091);
#2493=LINE('',#33848,#4092);
#2494=LINE('',#33849,#4093);
#2495=LINE('',#33851,#4094);
#2496=LINE('',#33855,#4095);
#2497=LINE('',#33857,#4096);
#2498=LINE('',#33859,#4097);
#2499=LINE('',#33860,#4098);
#2500=LINE('',#33863,#4099);
#2501=LINE('',#33865,#4100);
#2502=LINE('',#33866,#4101);
#2503=LINE('',#33869,#4102);
#2504=LINE('',#33871,#4103);
#2505=LINE('',#33872,#4104);
#2506=LINE('',#33874,#4105);
#2507=LINE('',#33876,#4106);
#2508=LINE('',#33878,#4107);
#2509=LINE('',#33879,#4108);
#2510=LINE('',#33881,#4109);
#2511=LINE('',#33882,#4110);
#2512=LINE('',#33883,#4111);
#2513=LINE('',#33886,#4112);
#2514=LINE('',#33889,#4113);
#2515=LINE('',#33891,#4114);
#2516=LINE('',#33893,#4115);
#2517=LINE('',#33894,#4116);
#2518=LINE('',#33897,#4117);
#2519=LINE('',#33898,#4118);
#2520=LINE('',#33901,#4119);
#2521=LINE('',#33903,#4120);
#2522=LINE('',#33904,#4121);
#2523=LINE('',#33905,#4122);
#2524=LINE('',#33908,#4123);
#2525=LINE('',#33909,#4124);
#2526=LINE('',#33911,#4125);
#2527=LINE('',#33913,#4126);
#2528=LINE('',#33915,#4127);
#3962=VECTOR('',#27448,1.);
#3963=VECTOR('',#27449,1.);
#3964=VECTOR('',#27450,1.);
#3965=VECTOR('',#27451,1.);
#3966=VECTOR('',#27454,1.);
#3967=VECTOR('',#27455,1.);
#3968=VECTOR('',#27456,1.);
#3969=VECTOR('',#27459,1.);
#3970=VECTOR('',#27460,1.);
#3971=VECTOR('',#27461,1.);
#3972=VECTOR('',#27464,1.);
#3973=VECTOR('',#27465,1.);
#3974=VECTOR('',#27468,1.);
#3975=VECTOR('',#27469,1.);
#3976=VECTOR('',#27470,1.);
#3977=VECTOR('',#27471,1.);
#3978=VECTOR('',#27474,1.);
#3979=VECTOR('',#27475,1.);
#3980=VECTOR('',#27476,1.);
#3981=VECTOR('',#27479,1.);
#3982=VECTOR('',#27480,1.);
#3983=VECTOR('',#27481,1.);
#3984=VECTOR('',#27484,1.);
#3985=VECTOR('',#27485,1.);
#3986=VECTOR('',#27488,1.);
#3987=VECTOR('',#27489,1.);
#3988=VECTOR('',#27490,1.);
#3989=VECTOR('',#27491,1.);
#3990=VECTOR('',#27494,1.);
#3991=VECTOR('',#27495,1.);
#3992=VECTOR('',#27496,1.);
#3993=VECTOR('',#27499,1.);
#3994=VECTOR('',#27500,1.);
#3995=VECTOR('',#27501,1.);
#3996=VECTOR('',#27504,1.);
#3997=VECTOR('',#27505,1.);
#3998=VECTOR('',#27508,1.);
#3999=VECTOR('',#27509,1.);
#4000=VECTOR('',#27510,1.);
#4001=VECTOR('',#27511,1.);
#4002=VECTOR('',#27514,1.);
#4003=VECTOR('',#27515,1.);
#4004=VECTOR('',#27516,1.);
#4005=VECTOR('',#27519,1.);
#4006=VECTOR('',#27520,1.);
#4007=VECTOR('',#27521,1.);
#4008=VECTOR('',#27524,1.);
#4009=VECTOR('',#27525,1.);
#4010=VECTOR('',#27528,1.);
#4011=VECTOR('',#27529,1.);
#4012=VECTOR('',#27530,1.);
#4013=VECTOR('',#27531,1.);
#4014=VECTOR('',#27534,1.);
#4015=VECTOR('',#27535,1.);
#4016=VECTOR('',#27536,1.);
#4017=VECTOR('',#27539,1.);
#4018=VECTOR('',#27540,1.);
#4019=VECTOR('',#27541,1.);
#4020=VECTOR('',#27544,1.);
#4021=VECTOR('',#27545,1.);
#4022=VECTOR('',#27548,1.);
#4023=VECTOR('',#27549,1.);
#4024=VECTOR('',#27550,1.);
#4025=VECTOR('',#27551,1.);
#4026=VECTOR('',#27554,1.);
#4027=VECTOR('',#27555,1.);
#4028=VECTOR('',#27556,1.);
#4029=VECTOR('',#27559,1.);
#4030=VECTOR('',#27560,1.);
#4031=VECTOR('',#27561,1.);
#4032=VECTOR('',#27564,1.);
#4033=VECTOR('',#27565,1.);
#4034=VECTOR('',#27568,1.);
#4035=VECTOR('',#27569,1.);
#4036=VECTOR('',#27570,1.);
#4037=VECTOR('',#27571,1.);
#4038=VECTOR('',#27574,1.);
#4039=VECTOR('',#27575,1.);
#4040=VECTOR('',#27576,1.);
#4041=VECTOR('',#27579,1.);
#4042=VECTOR('',#27580,1.);
#4043=VECTOR('',#27581,1.);
#4044=VECTOR('',#27584,1.);
#4045=VECTOR('',#27585,1.);
#4046=VECTOR('',#27586,1.);
#4047=VECTOR('',#27587,1.);
#4048=VECTOR('',#27588,1.);
#4049=VECTOR('',#27591,1.);
#4050=VECTOR('',#27592,1.);
#4051=VECTOR('',#27593,1.);
#4052=VECTOR('',#27594,1.);
#4053=VECTOR('',#27597,1.);
#4054=VECTOR('',#27598,1.);
#4055=VECTOR('',#27599,1.);
#4056=VECTOR('',#27602,1.);
#4057=VECTOR('',#27603,1.);
#4058=VECTOR('',#27604,1.);
#4059=VECTOR('',#27605,1.);
#4060=VECTOR('',#27606,1.);
#4061=VECTOR('',#27607,1.);
#4062=VECTOR('',#27608,1.);
#4063=VECTOR('',#27609,1.);
#4064=VECTOR('',#27610,1.);
#4065=VECTOR('',#27611,1.);
#4066=VECTOR('',#27614,1.);
#4067=VECTOR('',#27615,1.);
#4068=VECTOR('',#27616,1.);
#4069=VECTOR('',#27619,1.);
#4070=VECTOR('',#27620,1.);
#4071=VECTOR('',#27621,1.);
#4072=VECTOR('',#27622,1.);
#4073=VECTOR('',#27625,1.);
#4074=VECTOR('',#27626,1.);
#4075=VECTOR('',#27629,1.);
#4076=VECTOR('',#27630,1.);
#4077=VECTOR('',#27631,1.);
#4078=VECTOR('',#27632,1.);
#4079=VECTOR('',#27635,1.);
#4080=VECTOR('',#27636,1.);
#4081=VECTOR('',#27637,1.);
#4082=VECTOR('',#27638,1.);
#4083=VECTOR('',#27639,1.);
#4084=VECTOR('',#27640,1.);
#4085=VECTOR('',#27641,1.);
#4086=VECTOR('',#27642,1.);
#4087=VECTOR('',#27643,1.);
#4088=VECTOR('',#27646,1.);
#4089=VECTOR('',#27647,1.);
#4090=VECTOR('',#27648,1.);
#4091=VECTOR('',#27651,1.);
#4092=VECTOR('',#27652,1.);
#4093=VECTOR('',#27653,1.);
#4094=VECTOR('',#27656,1.);
#4095=VECTOR('',#27659,1.);
#4096=VECTOR('',#27660,1.);
#4097=VECTOR('',#27661,1.);
#4098=VECTOR('',#27662,1.);
#4099=VECTOR('',#27665,1.);
#4100=VECTOR('',#27666,1.);
#4101=VECTOR('',#27667,1.);
#4102=VECTOR('',#27670,1.);
#4103=VECTOR('',#27671,1.);
#4104=VECTOR('',#27672,1.);
#4105=VECTOR('',#27675,1.);
#4106=VECTOR('',#27676,1.);
#4107=VECTOR('',#27677,1.);
#4108=VECTOR('',#27678,1.);
#4109=VECTOR('',#27681,1.);
#4110=VECTOR('',#27682,1.);
#4111=VECTOR('',#27683,1.);
#4112=VECTOR('',#27688,1.);
#4113=VECTOR('',#27691,1.);
#4114=VECTOR('',#27692,1.);
#4115=VECTOR('',#27693,1.);
#4116=VECTOR('',#27694,1.);
#4117=VECTOR('',#27697,1.);
#4118=VECTOR('',#27698,1.);
#4119=VECTOR('',#27701,1.);
#4120=VECTOR('',#27702,1.);
#4121=VECTOR('',#27703,1.);
#4122=VECTOR('',#27704,1.);
#4123=VECTOR('',#27707,1.);
#4124=VECTOR('',#27708,1.);
#4125=VECTOR('',#27711,1.);
#4126=VECTOR('',#27714,1.);
#4127=VECTOR('',#27717,1.);
#5663=FACE_OUTER_BOUND('',#6800,.T.);
#5664=FACE_OUTER_BOUND('',#6801,.T.);
#5665=FACE_OUTER_BOUND('',#6802,.T.);
#5666=FACE_OUTER_BOUND('',#6803,.T.);
#5667=FACE_OUTER_BOUND('',#6804,.T.);
#5668=FACE_OUTER_BOUND('',#6805,.T.);
#5669=FACE_OUTER_BOUND('',#6806,.T.);
#5670=FACE_OUTER_BOUND('',#6807,.T.);
#5671=FACE_OUTER_BOUND('',#6808,.T.);
#5672=FACE_OUTER_BOUND('',#6809,.T.);
#5673=FACE_OUTER_BOUND('',#6810,.T.);
#5674=FACE_OUTER_BOUND('',#6811,.T.);
#5675=FACE_OUTER_BOUND('',#6812,.T.);
#5676=FACE_OUTER_BOUND('',#6813,.T.);
#5677=FACE_OUTER_BOUND('',#6814,.T.);
#5678=FACE_OUTER_BOUND('',#6815,.T.);
#5679=FACE_OUTER_BOUND('',#6816,.T.);
#5680=FACE_OUTER_BOUND('',#6817,.T.);
#5681=FACE_OUTER_BOUND('',#6818,.T.);
#5682=FACE_OUTER_BOUND('',#6819,.T.);
#5683=FACE_OUTER_BOUND('',#6820,.T.);
#5684=FACE_OUTER_BOUND('',#6821,.T.);
#5685=FACE_OUTER_BOUND('',#6822,.T.);
#5686=FACE_OUTER_BOUND('',#6823,.T.);
#5687=FACE_OUTER_BOUND('',#6824,.T.);
#5688=FACE_OUTER_BOUND('',#6825,.T.);
#5689=FACE_OUTER_BOUND('',#6826,.T.);
#5690=FACE_OUTER_BOUND('',#6827,.T.);
#5691=FACE_OUTER_BOUND('',#6828,.T.);
#5692=FACE_OUTER_BOUND('',#6829,.T.);
#5693=FACE_OUTER_BOUND('',#6830,.T.);
#5694=FACE_OUTER_BOUND('',#6837,.T.);
#5695=FACE_OUTER_BOUND('',#6838,.T.);
#5696=FACE_OUTER_BOUND('',#6839,.T.);
#5697=FACE_OUTER_BOUND('',#6840,.T.);
#5698=FACE_OUTER_BOUND('',#6841,.T.);
#5699=FACE_OUTER_BOUND('',#6842,.T.);
#5700=FACE_OUTER_BOUND('',#6843,.T.);
#5701=FACE_OUTER_BOUND('',#6844,.T.);
#5702=FACE_OUTER_BOUND('',#6845,.T.);
#5703=FACE_OUTER_BOUND('',#6846,.T.);
#5704=FACE_OUTER_BOUND('',#6847,.T.);
#5705=FACE_OUTER_BOUND('',#6848,.T.);
#5706=FACE_OUTER_BOUND('',#6849,.T.);
#5707=FACE_OUTER_BOUND('',#6850,.T.);
#5708=FACE_OUTER_BOUND('',#6851,.T.);
#5709=FACE_OUTER_BOUND('',#6852,.T.);
#5710=FACE_OUTER_BOUND('',#6853,.T.);
#5711=FACE_OUTER_BOUND('',#6854,.T.);
#5712=FACE_OUTER_BOUND('',#6855,.T.);
#5713=FACE_OUTER_BOUND('',#6856,.T.);
#5714=FACE_OUTER_BOUND('',#6857,.T.);
#5715=FACE_OUTER_BOUND('',#6864,.T.);
#5716=FACE_OUTER_BOUND('',#6865,.T.);
#6800=EDGE_LOOP('',(#17522,#17523,#17524,#17525));
#6801=EDGE_LOOP('',(#17526,#17527,#17528,#17529));
#6802=EDGE_LOOP('',(#17530,#17531,#17532,#17533));
#6803=EDGE_LOOP('',(#17534,#17535,#17536,#17537));
#6804=EDGE_LOOP('',(#17538,#17539,#17540,#17541));
#6805=EDGE_LOOP('',(#17542,#17543,#17544,#17545));
#6806=EDGE_LOOP('',(#17546,#17547,#17548,#17549));
#6807=EDGE_LOOP('',(#17550,#17551,#17552,#17553));
#6808=EDGE_LOOP('',(#17554,#17555,#17556,#17557));
#6809=EDGE_LOOP('',(#17558,#17559,#17560,#17561));
#6810=EDGE_LOOP('',(#17562,#17563,#17564,#17565));
#6811=EDGE_LOOP('',(#17566,#17567,#17568,#17569));
#6812=EDGE_LOOP('',(#17570,#17571,#17572,#17573));
#6813=EDGE_LOOP('',(#17574,#17575,#17576,#17577));
#6814=EDGE_LOOP('',(#17578,#17579,#17580,#17581));
#6815=EDGE_LOOP('',(#17582,#17583,#17584,#17585));
#6816=EDGE_LOOP('',(#17586,#17587,#17588,#17589));
#6817=EDGE_LOOP('',(#17590,#17591,#17592,#17593));
#6818=EDGE_LOOP('',(#17594,#17595,#17596,#17597));
#6819=EDGE_LOOP('',(#17598,#17599,#17600,#17601));
#6820=EDGE_LOOP('',(#17602,#17603,#17604,#17605));
#6821=EDGE_LOOP('',(#17606,#17607,#17608,#17609));
#6822=EDGE_LOOP('',(#17610,#17611,#17612,#17613));
#6823=EDGE_LOOP('',(#17614,#17615,#17616,#17617));
#6824=EDGE_LOOP('',(#17618,#17619,#17620,#17621));
#6825=EDGE_LOOP('',(#17622,#17623,#17624,#17625));
#6826=EDGE_LOOP('',(#17626,#17627,#17628,#17629));
#6827=EDGE_LOOP('',(#17630,#17631,#17632,#17633,#17634,#17635,#17636,#17637));
#6828=EDGE_LOOP('',(#17638,#17639,#17640,#17641,#17642,#17643));
#6829=EDGE_LOOP('',(#17644,#17645,#17646,#17647));
#6830=EDGE_LOOP('',(#17648,#17649,#17650,#17651,#17652,#17653,#17654,#17655,
#17656,#17657,#17658,#17659));
#6831=EDGE_LOOP('',(#17660,#17661,#17662,#17663));
#6832=EDGE_LOOP('',(#17664,#17665,#17666,#17667));
#6833=EDGE_LOOP('',(#17668,#17669,#17670,#17671));
#6834=EDGE_LOOP('',(#17672,#17673,#17674,#17675));
#6835=EDGE_LOOP('',(#17676,#17677,#17678,#17679));
#6836=EDGE_LOOP('',(#17680,#17681,#17682,#17683));
#6837=EDGE_LOOP('',(#17684,#17685,#17686,#17687));
#6838=EDGE_LOOP('',(#17688,#17689,#17690,#17691));
#6839=EDGE_LOOP('',(#17692,#17693,#17694,#17695,#17696));
#6840=EDGE_LOOP('',(#17697,#17698,#17699,#17700,#17701,#17702));
#6841=EDGE_LOOP('',(#17703,#17704,#17705,#17706,#17707,#17708,#17709,#17710,
#17711,#17712,#17713,#17714,#17715,#17716,#17717,#17718));
#6842=EDGE_LOOP('',(#17719,#17720,#17721,#17722));
#6843=EDGE_LOOP('',(#17723,#17724,#17725,#17726));
#6844=EDGE_LOOP('',(#17727,#17728,#17729,#17730,#17731));
#6845=EDGE_LOOP('',(#17732,#17733,#17734,#17735));
#6846=EDGE_LOOP('',(#17736,#17737,#17738,#17739));
#6847=EDGE_LOOP('',(#17740,#17741,#17742,#17743));
#6848=EDGE_LOOP('',(#17744,#17745,#17746,#17747,#17748,#17749,#17750,#17751));
#6849=EDGE_LOOP('',(#17752,#17753,#17754,#17755,#17756,#17757));
#6850=EDGE_LOOP('',(#17758,#17759,#17760,#17761,#17762,#17763,#17764,#17765));
#6851=EDGE_LOOP('',(#17766,#17767,#17768,#17769));
#6852=EDGE_LOOP('',(#17770,#17771,#17772,#17773,#17774,#17775,#17776,#17777,
#17778,#17779,#17780,#17781,#17782,#17783));
#6853=EDGE_LOOP('',(#17784,#17785,#17786,#17787));
#6854=EDGE_LOOP('',(#17788,#17789,#17790,#17791,#17792,#17793,#17794,#17795,
#17796,#17797,#17798,#17799,#17800,#17801));
#6855=EDGE_LOOP('',(#17802,#17803,#17804,#17805,#17806,#17807));
#6856=EDGE_LOOP('',(#17808,#17809,#17810,#17811));
#6857=EDGE_LOOP('',(#17812,#17813,#17814,#17815,#17816,#17817,#17818,#17819,
#17820,#17821));
#6858=EDGE_LOOP('',(#17822,#17823,#17824,#17825));
#6859=EDGE_LOOP('',(#17826,#17827,#17828,#17829));
#6860=EDGE_LOOP('',(#17830,#17831,#17832,#17833));
#6861=EDGE_LOOP('',(#17834,#17835,#17836,#17837));
#6862=EDGE_LOOP('',(#17838,#17839,#17840,#17841));
#6863=EDGE_LOOP('',(#17842,#17843,#17844,#17845));
#6864=EDGE_LOOP('',(#17846,#17847,#17848,#17849));
#6865=EDGE_LOOP('',(#17850,#17851,#17852,#17853));
#9637=VERTEX_POINT('',#33588);
#9638=VERTEX_POINT('',#33589);
#9639=VERTEX_POINT('',#33591);
#9640=VERTEX_POINT('',#33593);
#9641=VERTEX_POINT('',#33597);
#9642=VERTEX_POINT('',#33599);
#9643=VERTEX_POINT('',#33603);
#9644=VERTEX_POINT('',#33605);
#9645=VERTEX_POINT('',#33612);
#9646=VERTEX_POINT('',#33613);
#9647=VERTEX_POINT('',#33615);
#9648=VERTEX_POINT('',#33617);
#9649=VERTEX_POINT('',#33621);
#9650=VERTEX_POINT('',#33623);
#9651=VERTEX_POINT('',#33627);
#9652=VERTEX_POINT('',#33629);
#9653=VERTEX_POINT('',#33636);
#9654=VERTEX_POINT('',#33637);
#9655=VERTEX_POINT('',#33639);
#9656=VERTEX_POINT('',#33641);
#9657=VERTEX_POINT('',#33645);
#9658=VERTEX_POINT('',#33647);
#9659=VERTEX_POINT('',#33651);
#9660=VERTEX_POINT('',#33653);
#9661=VERTEX_POINT('',#33660);
#9662=VERTEX_POINT('',#33661);
#9663=VERTEX_POINT('',#33663);
#9664=VERTEX_POINT('',#33665);
#9665=VERTEX_POINT('',#33669);
#9666=VERTEX_POINT('',#33671);
#9667=VERTEX_POINT('',#33675);
#9668=VERTEX_POINT('',#33677);
#9669=VERTEX_POINT('',#33684);
#9670=VERTEX_POINT('',#33685);
#9671=VERTEX_POINT('',#33687);
#9672=VERTEX_POINT('',#33689);
#9673=VERTEX_POINT('',#33693);
#9674=VERTEX_POINT('',#33695);
#9675=VERTEX_POINT('',#33699);
#9676=VERTEX_POINT('',#33701);
#9677=VERTEX_POINT('',#33708);
#9678=VERTEX_POINT('',#33709);
#9679=VERTEX_POINT('',#33711);
#9680=VERTEX_POINT('',#33713);
#9681=VERTEX_POINT('',#33717);
#9682=VERTEX_POINT('',#33719);
#9683=VERTEX_POINT('',#33723);
#9684=VERTEX_POINT('',#33725);
#9685=VERTEX_POINT('',#33732);
#9686=VERTEX_POINT('',#33733);
#9687=VERTEX_POINT('',#33735);
#9688=VERTEX_POINT('',#33737);
#9689=VERTEX_POINT('',#33741);
#9690=VERTEX_POINT('',#33743);
#9691=VERTEX_POINT('',#33747);
#9692=VERTEX_POINT('',#33749);
#9693=VERTEX_POINT('',#33753);
#9694=VERTEX_POINT('',#33755);
#9695=VERTEX_POINT('',#33757);
#9696=VERTEX_POINT('',#33759);
#9697=VERTEX_POINT('',#33763);
#9698=VERTEX_POINT('',#33765);
#9699=VERTEX_POINT('',#33767);
#9700=VERTEX_POINT('',#33771);
#9701=VERTEX_POINT('',#33773);
#9702=VERTEX_POINT('',#33777);
#9703=VERTEX_POINT('',#33779);
#9704=VERTEX_POINT('',#33781);
#9705=VERTEX_POINT('',#33783);
#9706=VERTEX_POINT('',#33785);
#9707=VERTEX_POINT('',#33787);
#9708=VERTEX_POINT('',#33789);
#9709=VERTEX_POINT('',#33791);
#9710=VERTEX_POINT('',#33793);
#9711=VERTEX_POINT('',#33797);
#9712=VERTEX_POINT('',#33798);
#9713=VERTEX_POINT('',#33803);
#9714=VERTEX_POINT('',#33804);
#9715=VERTEX_POINT('',#33806);
#9716=VERTEX_POINT('',#33808);
#9717=VERTEX_POINT('',#33815);
#9718=VERTEX_POINT('',#33817);
#9719=VERTEX_POINT('',#33819);
#9720=VERTEX_POINT('',#33824);
#9721=VERTEX_POINT('',#33826);
#9722=VERTEX_POINT('',#33829);
#9723=VERTEX_POINT('',#33831);
#9724=VERTEX_POINT('',#33833);
#9725=VERTEX_POINT('',#33835);
#9726=VERTEX_POINT('',#33839);
#9727=VERTEX_POINT('',#33840);
#9728=VERTEX_POINT('',#33845);
#9729=VERTEX_POINT('',#33847);
#9730=VERTEX_POINT('',#33853);
#9731=VERTEX_POINT('',#33854);
#9732=VERTEX_POINT('',#33856);
#9733=VERTEX_POINT('',#33858);
#9734=VERTEX_POINT('',#33862);
#9735=VERTEX_POINT('',#33864);
#9736=VERTEX_POINT('',#33868);
#9737=VERTEX_POINT('',#33870);
#9738=VERTEX_POINT('',#33875);
#9739=VERTEX_POINT('',#33877);
#9740=VERTEX_POINT('',#33888);
#9741=VERTEX_POINT('',#33890);
#9742=VERTEX_POINT('',#33892);
#9743=VERTEX_POINT('',#33896);
#9744=VERTEX_POINT('',#33900);
#9745=VERTEX_POINT('',#33902);
#9746=VERTEX_POINT('',#33907);
#12319=EDGE_CURVE('',#9637,#9638,#2363,.T.);
#12320=EDGE_CURVE('',#9639,#9637,#2364,.T.);
#12321=EDGE_CURVE('',#9640,#9639,#2365,.T.);
#12322=EDGE_CURVE('',#9640,#9638,#2366,.T.);
#12323=EDGE_CURVE('',#9638,#9641,#2367,.T.);
#12324=EDGE_CURVE('',#9642,#9640,#2368,.T.);
#12325=EDGE_CURVE('',#9642,#9641,#2369,.T.);
#12326=EDGE_CURVE('',#9641,#9643,#2370,.T.);
#12327=EDGE_CURVE('',#9644,#9642,#2371,.T.);
#12328=EDGE_CURVE('',#9644,#9643,#2372,.T.);
#12329=EDGE_CURVE('',#9643,#9637,#2373,.T.);
#12330=EDGE_CURVE('',#9639,#9644,#2374,.T.);
#12331=EDGE_CURVE('',#9645,#9646,#2375,.T.);
#12332=EDGE_CURVE('',#9647,#9645,#2376,.T.);
#12333=EDGE_CURVE('',#9648,#9647,#2377,.T.);
#12334=EDGE_CURVE('',#9648,#9646,#2378,.T.);
#12335=EDGE_CURVE('',#9646,#9649,#2379,.T.);
#12336=EDGE_CURVE('',#9650,#9648,#2380,.T.);
#12337=EDGE_CURVE('',#9650,#9649,#2381,.T.);
#12338=EDGE_CURVE('',#9649,#9651,#2382,.T.);
#12339=EDGE_CURVE('',#9652,#9650,#2383,.T.);
#12340=EDGE_CURVE('',#9652,#9651,#2384,.T.);
#12341=EDGE_CURVE('',#9651,#9645,#2385,.T.);
#12342=EDGE_CURVE('',#9647,#9652,#2386,.T.);
#12343=EDGE_CURVE('',#9653,#9654,#2387,.T.);
#12344=EDGE_CURVE('',#9655,#9653,#2388,.T.);
#12345=EDGE_CURVE('',#9656,#9655,#2389,.T.);
#12346=EDGE_CURVE('',#9656,#9654,#2390,.T.);
#12347=EDGE_CURVE('',#9654,#9657,#2391,.T.);
#12348=EDGE_CURVE('',#9658,#9656,#2392,.T.);
#12349=EDGE_CURVE('',#9658,#9657,#2393,.T.);
#12350=EDGE_CURVE('',#9657,#9659,#2394,.T.);
#12351=EDGE_CURVE('',#9660,#9658,#2395,.T.);
#12352=EDGE_CURVE('',#9660,#9659,#2396,.T.);
#12353=EDGE_CURVE('',#9659,#9653,#2397,.T.);
#12354=EDGE_CURVE('',#9655,#9660,#2398,.T.);
#12355=EDGE_CURVE('',#9661,#9662,#2399,.T.);
#12356=EDGE_CURVE('',#9663,#9661,#2400,.T.);
#12357=EDGE_CURVE('',#9664,#9663,#2401,.T.);
#12358=EDGE_CURVE('',#9664,#9662,#2402,.T.);
#12359=EDGE_CURVE('',#9662,#9665,#2403,.T.);
#12360=EDGE_CURVE('',#9666,#9664,#2404,.T.);
#12361=EDGE_CURVE('',#9666,#9665,#2405,.T.);
#12362=EDGE_CURVE('',#9665,#9667,#2406,.T.);
#12363=EDGE_CURVE('',#9668,#9666,#2407,.T.);
#12364=EDGE_CURVE('',#9668,#9667,#2408,.T.);
#12365=EDGE_CURVE('',#9667,#9661,#2409,.T.);
#12366=EDGE_CURVE('',#9663,#9668,#2410,.T.);
#12367=EDGE_CURVE('',#9669,#9670,#2411,.T.);
#12368=EDGE_CURVE('',#9671,#9669,#2412,.T.);
#12369=EDGE_CURVE('',#9672,#9671,#2413,.T.);
#12370=EDGE_CURVE('',#9672,#9670,#2414,.T.);
#12371=EDGE_CURVE('',#9670,#9673,#2415,.T.);
#12372=EDGE_CURVE('',#9674,#9672,#2416,.T.);
#12373=EDGE_CURVE('',#9674,#9673,#2417,.T.);
#12374=EDGE_CURVE('',#9673,#9675,#2418,.T.);
#12375=EDGE_CURVE('',#9676,#9674,#2419,.T.);
#12376=EDGE_CURVE('',#9676,#9675,#2420,.T.);
#12377=EDGE_CURVE('',#9675,#9669,#2421,.T.);
#12378=EDGE_CURVE('',#9671,#9676,#2422,.T.);
#12379=EDGE_CURVE('',#9677,#9678,#2423,.T.);
#12380=EDGE_CURVE('',#9679,#9677,#2424,.T.);
#12381=EDGE_CURVE('',#9680,#9679,#2425,.T.);
#12382=EDGE_CURVE('',#9680,#9678,#2426,.T.);
#12383=EDGE_CURVE('',#9678,#9681,#2427,.T.);
#12384=EDGE_CURVE('',#9682,#9680,#2428,.T.);
#12385=EDGE_CURVE('',#9682,#9681,#2429,.T.);
#12386=EDGE_CURVE('',#9681,#9683,#2430,.T.);
#12387=EDGE_CURVE('',#9684,#9682,#2431,.T.);
#12388=EDGE_CURVE('',#9684,#9683,#2432,.T.);
#12389=EDGE_CURVE('',#9683,#9677,#2433,.T.);
#12390=EDGE_CURVE('',#9679,#9684,#2434,.T.);
#12391=EDGE_CURVE('',#9685,#9686,#2435,.T.);
#12392=EDGE_CURVE('',#9687,#9685,#2436,.T.);
#12393=EDGE_CURVE('',#9687,#9688,#2437,.T.);
#12394=EDGE_CURVE('',#9686,#9688,#2438,.T.);
#12395=EDGE_CURVE('',#9689,#9687,#2439,.T.);
#12396=EDGE_CURVE('',#9690,#9689,#2440,.T.);
#12397=EDGE_CURVE('',#9688,#9690,#2441,.T.);
#12398=EDGE_CURVE('',#9685,#9691,#2442,.T.);
#12399=EDGE_CURVE('',#9692,#9686,#2443,.T.);
#12400=EDGE_CURVE('',#9691,#9692,#2444,.T.);
#12401=EDGE_CURVE('',#9693,#9690,#2445,.T.);
#12402=EDGE_CURVE('',#9694,#9693,#2446,.T.);
#12403=EDGE_CURVE('',#9695,#9694,#2447,.T.);
#12404=EDGE_CURVE('',#9695,#9696,#2448,.T.);
#12405=EDGE_CURVE('',#9692,#9696,#2449,.T.);
#12406=EDGE_CURVE('',#9697,#9689,#2450,.T.);
#12407=EDGE_CURVE('',#9697,#9698,#2451,.T.);
#12408=EDGE_CURVE('',#9699,#9698,#2452,.T.);
#12409=EDGE_CURVE('',#9699,#9693,#2453,.T.);
#12410=EDGE_CURVE('',#9700,#9695,#2454,.T.);
#12411=EDGE_CURVE('',#9701,#9700,#2455,.T.);
#12412=EDGE_CURVE('',#9696,#9701,#2456,.T.);
#12413=EDGE_CURVE('',#9702,#9694,#2457,.T.);
#12414=EDGE_CURVE('',#9702,#9703,#2458,.T.);
#12415=EDGE_CURVE('',#9703,#9704,#2459,.T.);
#12416=EDGE_CURVE('',#9704,#9705,#2460,.T.);
#12417=EDGE_CURVE('',#9706,#9705,#2461,.T.);
#12418=EDGE_CURVE('',#9706,#9707,#2462,.T.);
#12419=EDGE_CURVE('',#9707,#9708,#2463,.T.);
#12420=EDGE_CURVE('',#9708,#9709,#2464,.T.);
#12421=EDGE_CURVE('',#9710,#9709,#2465,.T.);
#12422=EDGE_CURVE('',#9700,#9710,#2466,.T.);
#12423=EDGE_CURVE('',#9711,#9712,#2467,.T.);
#12424=EDGE_CURVE('',#9712,#9708,#2468,.T.);
#12425=EDGE_CURVE('',#9707,#9711,#2469,.T.);
#12426=EDGE_CURVE('',#9713,#9714,#2470,.T.);
#12427=EDGE_CURVE('',#9715,#9714,#2471,.T.);
#12428=EDGE_CURVE('',#9715,#9716,#2472,.T.);
#12429=EDGE_CURVE('',#9713,#9716,#2473,.T.);
#12430=EDGE_CURVE('',#9716,#9706,#2474,.T.);
#12431=EDGE_CURVE('',#9711,#9715,#2475,.T.);
#12432=EDGE_CURVE('',#9714,#9717,#2476,.T.);
#12433=EDGE_CURVE('',#9718,#9717,#2477,.T.);
#12434=EDGE_CURVE('',#9719,#9718,#2478,.T.);
#12435=EDGE_CURVE('',#9719,#9711,#2479,.T.);
#12436=EDGE_CURVE('',#9709,#9713,#2480,.T.);
#12437=EDGE_CURVE('',#9705,#9720,#2481,.T.);
#12438=EDGE_CURVE('',#9720,#9721,#2482,.T.);
#12439=EDGE_CURVE('',#9721,#9702,#2483,.T.);
#12440=EDGE_CURVE('',#9722,#9699,#2484,.T.);
#12441=EDGE_CURVE('',#9723,#9722,#2485,.T.);
#12442=EDGE_CURVE('',#9724,#9723,#2486,.T.);
#12443=EDGE_CURVE('',#9725,#9724,#2487,.T.);
#12444=EDGE_CURVE('',#9710,#9725,#2488,.T.);
#12445=EDGE_CURVE('',#9726,#9727,#2489,.T.);
#12446=EDGE_CURVE('',#9727,#9704,#2490,.T.);
#12447=EDGE_CURVE('',#9726,#9703,#2491,.T.);
#12448=EDGE_CURVE('',#9721,#9728,#2492,.T.);
#12449=EDGE_CURVE('',#9720,#9729,#2493,.T.);
#12450=EDGE_CURVE('',#9728,#9729,#2494,.T.);
#12451=EDGE_CURVE('',#9729,#9727,#2495,.T.);
#12452=EDGE_CURVE('',#9730,#9731,#2496,.T.);
#12453=EDGE_CURVE('',#9732,#9731,#2497,.T.);
#12454=EDGE_CURVE('',#9732,#9733,#2498,.T.);
#12455=EDGE_CURVE('',#9730,#9733,#2499,.T.);
#12456=EDGE_CURVE('',#9734,#9730,#2500,.T.);
#12457=EDGE_CURVE('',#9735,#9734,#2501,.T.);
#12458=EDGE_CURVE('',#9731,#9735,#2502,.T.);
#12459=EDGE_CURVE('',#9733,#9736,#2503,.T.);
#12460=EDGE_CURVE('',#9737,#9732,#2504,.T.);
#12461=EDGE_CURVE('',#9736,#9737,#2505,.T.);
#12462=EDGE_CURVE('',#9736,#9701,#2506,.T.);
#12463=EDGE_CURVE('',#9737,#9738,#2507,.T.);
#12464=EDGE_CURVE('',#9739,#9738,#2508,.T.);
#12465=EDGE_CURVE('',#9691,#9739,#2509,.T.);
#12466=EDGE_CURVE('',#9725,#9734,#2510,.T.);
#12467=EDGE_CURVE('',#9724,#9718,#2511,.T.);
#12468=EDGE_CURVE('',#9717,#9735,#2512,.T.);
#12469=EDGE_CURVE('',#9723,#9719,#2513,.T.);
#12470=EDGE_CURVE('',#9740,#9712,#2514,.T.);
#12471=EDGE_CURVE('',#9741,#9740,#2515,.T.);
#12472=EDGE_CURVE('',#9742,#9741,#2516,.T.);
#12473=EDGE_CURVE('',#9738,#9742,#2517,.T.);
#12474=EDGE_CURVE('',#9743,#9742,#2518,.T.);
#12475=EDGE_CURVE('',#9739,#9743,#2519,.T.);
#12476=EDGE_CURVE('',#9743,#9744,#2520,.T.);
#12477=EDGE_CURVE('',#9744,#9745,#2521,.T.);
#12478=EDGE_CURVE('',#9745,#9726,#2522,.T.);
#12479=EDGE_CURVE('',#9728,#9697,#2523,.T.);
#12480=EDGE_CURVE('',#9727,#9746,#2524,.T.);
#12481=EDGE_CURVE('',#9698,#9746,#2525,.T.);
#12482=EDGE_CURVE('',#9722,#9746,#2526,.T.);
#12483=EDGE_CURVE('',#9745,#9740,#2527,.T.);
#12484=EDGE_CURVE('',#9744,#9741,#2528,.T.);
#17522=ORIENTED_EDGE('',*,*,#12319,.F.);
#17523=ORIENTED_EDGE('',*,*,#12320,.F.);
#17524=ORIENTED_EDGE('',*,*,#12321,.F.);
#17525=ORIENTED_EDGE('',*,*,#12322,.T.);
#17526=ORIENTED_EDGE('',*,*,#12323,.F.);
#17527=ORIENTED_EDGE('',*,*,#12322,.F.);
#17528=ORIENTED_EDGE('',*,*,#12324,.F.);
#17529=ORIENTED_EDGE('',*,*,#12325,.T.);
#17530=ORIENTED_EDGE('',*,*,#12326,.F.);
#17531=ORIENTED_EDGE('',*,*,#12325,.F.);
#17532=ORIENTED_EDGE('',*,*,#12327,.F.);
#17533=ORIENTED_EDGE('',*,*,#12328,.T.);
#17534=ORIENTED_EDGE('',*,*,#12329,.F.);
#17535=ORIENTED_EDGE('',*,*,#12328,.F.);
#17536=ORIENTED_EDGE('',*,*,#12330,.F.);
#17537=ORIENTED_EDGE('',*,*,#12320,.T.);
#17538=ORIENTED_EDGE('',*,*,#12331,.F.);
#17539=ORIENTED_EDGE('',*,*,#12332,.F.);
#17540=ORIENTED_EDGE('',*,*,#12333,.F.);
#17541=ORIENTED_EDGE('',*,*,#12334,.T.);
#17542=ORIENTED_EDGE('',*,*,#12335,.F.);
#17543=ORIENTED_EDGE('',*,*,#12334,.F.);
#17544=ORIENTED_EDGE('',*,*,#12336,.F.);
#17545=ORIENTED_EDGE('',*,*,#12337,.T.);
#17546=ORIENTED_EDGE('',*,*,#12338,.F.);
#17547=ORIENTED_EDGE('',*,*,#12337,.F.);
#17548=ORIENTED_EDGE('',*,*,#12339,.F.);
#17549=ORIENTED_EDGE('',*,*,#12340,.T.);
#17550=ORIENTED_EDGE('',*,*,#12341,.F.);
#17551=ORIENTED_EDGE('',*,*,#12340,.F.);
#17552=ORIENTED_EDGE('',*,*,#12342,.F.);
#17553=ORIENTED_EDGE('',*,*,#12332,.T.);
#17554=ORIENTED_EDGE('',*,*,#12343,.F.);
#17555=ORIENTED_EDGE('',*,*,#12344,.F.);
#17556=ORIENTED_EDGE('',*,*,#12345,.F.);
#17557=ORIENTED_EDGE('',*,*,#12346,.T.);
#17558=ORIENTED_EDGE('',*,*,#12347,.F.);
#17559=ORIENTED_EDGE('',*,*,#12346,.F.);
#17560=ORIENTED_EDGE('',*,*,#12348,.F.);
#17561=ORIENTED_EDGE('',*,*,#12349,.T.);
#17562=ORIENTED_EDGE('',*,*,#12350,.F.);
#17563=ORIENTED_EDGE('',*,*,#12349,.F.);
#17564=ORIENTED_EDGE('',*,*,#12351,.F.);
#17565=ORIENTED_EDGE('',*,*,#12352,.T.);
#17566=ORIENTED_EDGE('',*,*,#12353,.F.);
#17567=ORIENTED_EDGE('',*,*,#12352,.F.);
#17568=ORIENTED_EDGE('',*,*,#12354,.F.);
#17569=ORIENTED_EDGE('',*,*,#12344,.T.);
#17570=ORIENTED_EDGE('',*,*,#12355,.F.);
#17571=ORIENTED_EDGE('',*,*,#12356,.F.);
#17572=ORIENTED_EDGE('',*,*,#12357,.F.);
#17573=ORIENTED_EDGE('',*,*,#12358,.T.);
#17574=ORIENTED_EDGE('',*,*,#12359,.F.);
#17575=ORIENTED_EDGE('',*,*,#12358,.F.);
#17576=ORIENTED_EDGE('',*,*,#12360,.F.);
#17577=ORIENTED_EDGE('',*,*,#12361,.T.);
#17578=ORIENTED_EDGE('',*,*,#12362,.F.);
#17579=ORIENTED_EDGE('',*,*,#12361,.F.);
#17580=ORIENTED_EDGE('',*,*,#12363,.F.);
#17581=ORIENTED_EDGE('',*,*,#12364,.T.);
#17582=ORIENTED_EDGE('',*,*,#12365,.F.);
#17583=ORIENTED_EDGE('',*,*,#12364,.F.);
#17584=ORIENTED_EDGE('',*,*,#12366,.F.);
#17585=ORIENTED_EDGE('',*,*,#12356,.T.);
#17586=ORIENTED_EDGE('',*,*,#12367,.F.);
#17587=ORIENTED_EDGE('',*,*,#12368,.F.);
#17588=ORIENTED_EDGE('',*,*,#12369,.F.);
#17589=ORIENTED_EDGE('',*,*,#12370,.T.);
#17590=ORIENTED_EDGE('',*,*,#12371,.F.);
#17591=ORIENTED_EDGE('',*,*,#12370,.F.);
#17592=ORIENTED_EDGE('',*,*,#12372,.F.);
#17593=ORIENTED_EDGE('',*,*,#12373,.T.);
#17594=ORIENTED_EDGE('',*,*,#12374,.F.);
#17595=ORIENTED_EDGE('',*,*,#12373,.F.);
#17596=ORIENTED_EDGE('',*,*,#12375,.F.);
#17597=ORIENTED_EDGE('',*,*,#12376,.T.);
#17598=ORIENTED_EDGE('',*,*,#12377,.F.);
#17599=ORIENTED_EDGE('',*,*,#12376,.F.);
#17600=ORIENTED_EDGE('',*,*,#12378,.F.);
#17601=ORIENTED_EDGE('',*,*,#12368,.T.);
#17602=ORIENTED_EDGE('',*,*,#12379,.F.);
#17603=ORIENTED_EDGE('',*,*,#12380,.F.);
#17604=ORIENTED_EDGE('',*,*,#12381,.F.);
#17605=ORIENTED_EDGE('',*,*,#12382,.T.);
#17606=ORIENTED_EDGE('',*,*,#12383,.F.);
#17607=ORIENTED_EDGE('',*,*,#12382,.F.);
#17608=ORIENTED_EDGE('',*,*,#12384,.F.);
#17609=ORIENTED_EDGE('',*,*,#12385,.T.);
#17610=ORIENTED_EDGE('',*,*,#12386,.F.);
#17611=ORIENTED_EDGE('',*,*,#12385,.F.);
#17612=ORIENTED_EDGE('',*,*,#12387,.F.);
#17613=ORIENTED_EDGE('',*,*,#12388,.T.);
#17614=ORIENTED_EDGE('',*,*,#12389,.F.);
#17615=ORIENTED_EDGE('',*,*,#12388,.F.);
#17616=ORIENTED_EDGE('',*,*,#12390,.F.);
#17617=ORIENTED_EDGE('',*,*,#12380,.T.);
#17618=ORIENTED_EDGE('',*,*,#12391,.F.);
#17619=ORIENTED_EDGE('',*,*,#12392,.F.);
#17620=ORIENTED_EDGE('',*,*,#12393,.T.);
#17621=ORIENTED_EDGE('',*,*,#12394,.F.);
#17622=ORIENTED_EDGE('',*,*,#12395,.F.);
#17623=ORIENTED_EDGE('',*,*,#12396,.F.);
#17624=ORIENTED_EDGE('',*,*,#12397,.F.);
#17625=ORIENTED_EDGE('',*,*,#12393,.F.);
#17626=ORIENTED_EDGE('',*,*,#12398,.F.);
#17627=ORIENTED_EDGE('',*,*,#12391,.T.);
#17628=ORIENTED_EDGE('',*,*,#12399,.F.);
#17629=ORIENTED_EDGE('',*,*,#12400,.F.);
#17630=ORIENTED_EDGE('',*,*,#12399,.T.);
#17631=ORIENTED_EDGE('',*,*,#12394,.T.);
#17632=ORIENTED_EDGE('',*,*,#12397,.T.);
#17633=ORIENTED_EDGE('',*,*,#12401,.F.);
#17634=ORIENTED_EDGE('',*,*,#12402,.F.);
#17635=ORIENTED_EDGE('',*,*,#12403,.F.);
#17636=ORIENTED_EDGE('',*,*,#12404,.T.);
#17637=ORIENTED_EDGE('',*,*,#12405,.F.);
#17638=ORIENTED_EDGE('',*,*,#12396,.T.);
#17639=ORIENTED_EDGE('',*,*,#12406,.F.);
#17640=ORIENTED_EDGE('',*,*,#12407,.T.);
#17641=ORIENTED_EDGE('',*,*,#12408,.F.);
#17642=ORIENTED_EDGE('',*,*,#12409,.T.);
#17643=ORIENTED_EDGE('',*,*,#12401,.T.);
#17644=ORIENTED_EDGE('',*,*,#12410,.F.);
#17645=ORIENTED_EDGE('',*,*,#12411,.F.);
#17646=ORIENTED_EDGE('',*,*,#12412,.F.);
#17647=ORIENTED_EDGE('',*,*,#12404,.F.);
#17648=ORIENTED_EDGE('',*,*,#12410,.T.);
#17649=ORIENTED_EDGE('',*,*,#12403,.T.);
#17650=ORIENTED_EDGE('',*,*,#12413,.F.);
#17651=ORIENTED_EDGE('',*,*,#12414,.T.);
#17652=ORIENTED_EDGE('',*,*,#12415,.T.);
#17653=ORIENTED_EDGE('',*,*,#12416,.T.);
#17654=ORIENTED_EDGE('',*,*,#12417,.F.);
#17655=ORIENTED_EDGE('',*,*,#12418,.T.);
#17656=ORIENTED_EDGE('',*,*,#12419,.T.);
#17657=ORIENTED_EDGE('',*,*,#12420,.T.);
#17658=ORIENTED_EDGE('',*,*,#12421,.F.);
#17659=ORIENTED_EDGE('',*,*,#12422,.F.);
#17660=ORIENTED_EDGE('',*,*,#12326,.T.);
#17661=ORIENTED_EDGE('',*,*,#12329,.T.);
#17662=ORIENTED_EDGE('',*,*,#12319,.T.);
#17663=ORIENTED_EDGE('',*,*,#12323,.T.);
#17664=ORIENTED_EDGE('',*,*,#12338,.T.);
#17665=ORIENTED_EDGE('',*,*,#12341,.T.);
#17666=ORIENTED_EDGE('',*,*,#12331,.T.);
#17667=ORIENTED_EDGE('',*,*,#12335,.T.);
#17668=ORIENTED_EDGE('',*,*,#12350,.T.);
#17669=ORIENTED_EDGE('',*,*,#12353,.T.);
#17670=ORIENTED_EDGE('',*,*,#12343,.T.);
#17671=ORIENTED_EDGE('',*,*,#12347,.T.);
#17672=ORIENTED_EDGE('',*,*,#12362,.T.);
#17673=ORIENTED_EDGE('',*,*,#12365,.T.);
#17674=ORIENTED_EDGE('',*,*,#12355,.T.);
#17675=ORIENTED_EDGE('',*,*,#12359,.T.);
#17676=ORIENTED_EDGE('',*,*,#12374,.T.);
#17677=ORIENTED_EDGE('',*,*,#12377,.T.);
#17678=ORIENTED_EDGE('',*,*,#12367,.T.);
#17679=ORIENTED_EDGE('',*,*,#12371,.T.);
#17680=ORIENTED_EDGE('',*,*,#12386,.T.);
#17681=ORIENTED_EDGE('',*,*,#12389,.T.);
#17682=ORIENTED_EDGE('',*,*,#12379,.T.);
#17683=ORIENTED_EDGE('',*,*,#12383,.T.);
#17684=ORIENTED_EDGE('',*,*,#12423,.T.);
#17685=ORIENTED_EDGE('',*,*,#12424,.T.);
#17686=ORIENTED_EDGE('',*,*,#12419,.F.);
#17687=ORIENTED_EDGE('',*,*,#12425,.T.);
#17688=ORIENTED_EDGE('',*,*,#12426,.T.);
#17689=ORIENTED_EDGE('',*,*,#12427,.F.);
#17690=ORIENTED_EDGE('',*,*,#12428,.T.);
#17691=ORIENTED_EDGE('',*,*,#12429,.F.);
#17692=ORIENTED_EDGE('',*,*,#12418,.F.);
#17693=ORIENTED_EDGE('',*,*,#12430,.F.);
#17694=ORIENTED_EDGE('',*,*,#12428,.F.);
#17695=ORIENTED_EDGE('',*,*,#12431,.F.);
#17696=ORIENTED_EDGE('',*,*,#12425,.F.);
#17697=ORIENTED_EDGE('',*,*,#12431,.T.);
#17698=ORIENTED_EDGE('',*,*,#12427,.T.);
#17699=ORIENTED_EDGE('',*,*,#12432,.T.);
#17700=ORIENTED_EDGE('',*,*,#12433,.F.);
#17701=ORIENTED_EDGE('',*,*,#12434,.F.);
#17702=ORIENTED_EDGE('',*,*,#12435,.T.);
#17703=ORIENTED_EDGE('',*,*,#12436,.T.);
#17704=ORIENTED_EDGE('',*,*,#12429,.T.);
#17705=ORIENTED_EDGE('',*,*,#12430,.T.);
#17706=ORIENTED_EDGE('',*,*,#12417,.T.);
#17707=ORIENTED_EDGE('',*,*,#12437,.T.);
#17708=ORIENTED_EDGE('',*,*,#12438,.T.);
#17709=ORIENTED_EDGE('',*,*,#12439,.T.);
#17710=ORIENTED_EDGE('',*,*,#12413,.T.);
#17711=ORIENTED_EDGE('',*,*,#12402,.T.);
#17712=ORIENTED_EDGE('',*,*,#12409,.F.);
#17713=ORIENTED_EDGE('',*,*,#12440,.F.);
#17714=ORIENTED_EDGE('',*,*,#12441,.F.);
#17715=ORIENTED_EDGE('',*,*,#12442,.F.);
#17716=ORIENTED_EDGE('',*,*,#12443,.F.);
#17717=ORIENTED_EDGE('',*,*,#12444,.F.);
#17718=ORIENTED_EDGE('',*,*,#12421,.T.);
#17719=ORIENTED_EDGE('',*,*,#12445,.T.);
#17720=ORIENTED_EDGE('',*,*,#12446,.T.);
#17721=ORIENTED_EDGE('',*,*,#12415,.F.);
#17722=ORIENTED_EDGE('',*,*,#12447,.F.);
#17723=ORIENTED_EDGE('',*,*,#12448,.F.);
#17724=ORIENTED_EDGE('',*,*,#12438,.F.);
#17725=ORIENTED_EDGE('',*,*,#12449,.T.);
#17726=ORIENTED_EDGE('',*,*,#12450,.F.);
#17727=ORIENTED_EDGE('',*,*,#12451,.F.);
#17728=ORIENTED_EDGE('',*,*,#12449,.F.);
#17729=ORIENTED_EDGE('',*,*,#12437,.F.);
#17730=ORIENTED_EDGE('',*,*,#12416,.F.);
#17731=ORIENTED_EDGE('',*,*,#12446,.F.);
#17732=ORIENTED_EDGE('',*,*,#12452,.T.);
#17733=ORIENTED_EDGE('',*,*,#12453,.F.);
#17734=ORIENTED_EDGE('',*,*,#12454,.T.);
#17735=ORIENTED_EDGE('',*,*,#12455,.F.);
#17736=ORIENTED_EDGE('',*,*,#12456,.F.);
#17737=ORIENTED_EDGE('',*,*,#12457,.F.);
#17738=ORIENTED_EDGE('',*,*,#12458,.F.);
#17739=ORIENTED_EDGE('',*,*,#12452,.F.);
#17740=ORIENTED_EDGE('',*,*,#12459,.F.);
#17741=ORIENTED_EDGE('',*,*,#12454,.F.);
#17742=ORIENTED_EDGE('',*,*,#12460,.F.);
#17743=ORIENTED_EDGE('',*,*,#12461,.F.);
#17744=ORIENTED_EDGE('',*,*,#12400,.T.);
#17745=ORIENTED_EDGE('',*,*,#12405,.T.);
#17746=ORIENTED_EDGE('',*,*,#12412,.T.);
#17747=ORIENTED_EDGE('',*,*,#12462,.F.);
#17748=ORIENTED_EDGE('',*,*,#12461,.T.);
#17749=ORIENTED_EDGE('',*,*,#12463,.T.);
#17750=ORIENTED_EDGE('',*,*,#12464,.F.);
#17751=ORIENTED_EDGE('',*,*,#12465,.F.);
#17752=ORIENTED_EDGE('',*,*,#12457,.T.);
#17753=ORIENTED_EDGE('',*,*,#12466,.F.);
#17754=ORIENTED_EDGE('',*,*,#12443,.T.);
#17755=ORIENTED_EDGE('',*,*,#12467,.T.);
#17756=ORIENTED_EDGE('',*,*,#12433,.T.);
#17757=ORIENTED_EDGE('',*,*,#12468,.T.);
#17758=ORIENTED_EDGE('',*,*,#12411,.T.);
#17759=ORIENTED_EDGE('',*,*,#12422,.T.);
#17760=ORIENTED_EDGE('',*,*,#12444,.T.);
#17761=ORIENTED_EDGE('',*,*,#12466,.T.);
#17762=ORIENTED_EDGE('',*,*,#12456,.T.);
#17763=ORIENTED_EDGE('',*,*,#12455,.T.);
#17764=ORIENTED_EDGE('',*,*,#12459,.T.);
#17765=ORIENTED_EDGE('',*,*,#12462,.T.);
#17766=ORIENTED_EDGE('',*,*,#12442,.T.);
#17767=ORIENTED_EDGE('',*,*,#12469,.T.);
#17768=ORIENTED_EDGE('',*,*,#12434,.T.);
#17769=ORIENTED_EDGE('',*,*,#12467,.F.);
#17770=ORIENTED_EDGE('',*,*,#12458,.T.);
#17771=ORIENTED_EDGE('',*,*,#12468,.F.);
#17772=ORIENTED_EDGE('',*,*,#12432,.F.);
#17773=ORIENTED_EDGE('',*,*,#12426,.F.);
#17774=ORIENTED_EDGE('',*,*,#12436,.F.);
#17775=ORIENTED_EDGE('',*,*,#12420,.F.);
#17776=ORIENTED_EDGE('',*,*,#12424,.F.);
#17777=ORIENTED_EDGE('',*,*,#12470,.F.);
#17778=ORIENTED_EDGE('',*,*,#12471,.F.);
#17779=ORIENTED_EDGE('',*,*,#12472,.F.);
#17780=ORIENTED_EDGE('',*,*,#12473,.F.);
#17781=ORIENTED_EDGE('',*,*,#12463,.F.);
#17782=ORIENTED_EDGE('',*,*,#12460,.T.);
#17783=ORIENTED_EDGE('',*,*,#12453,.T.);
#17784=ORIENTED_EDGE('',*,*,#12464,.T.);
#17785=ORIENTED_EDGE('',*,*,#12473,.T.);
#17786=ORIENTED_EDGE('',*,*,#12474,.F.);
#17787=ORIENTED_EDGE('',*,*,#12475,.F.);
#17788=ORIENTED_EDGE('',*,*,#12398,.T.);
#17789=ORIENTED_EDGE('',*,*,#12465,.T.);
#17790=ORIENTED_EDGE('',*,*,#12475,.T.);
#17791=ORIENTED_EDGE('',*,*,#12476,.T.);
#17792=ORIENTED_EDGE('',*,*,#12477,.T.);
#17793=ORIENTED_EDGE('',*,*,#12478,.T.);
#17794=ORIENTED_EDGE('',*,*,#12447,.T.);
#17795=ORIENTED_EDGE('',*,*,#12414,.F.);
#17796=ORIENTED_EDGE('',*,*,#12439,.F.);
#17797=ORIENTED_EDGE('',*,*,#12448,.T.);
#17798=ORIENTED_EDGE('',*,*,#12479,.T.);
#17799=ORIENTED_EDGE('',*,*,#12406,.T.);
#17800=ORIENTED_EDGE('',*,*,#12395,.T.);
#17801=ORIENTED_EDGE('',*,*,#12392,.T.);
#17802=ORIENTED_EDGE('',*,*,#12451,.T.);
#17803=ORIENTED_EDGE('',*,*,#12480,.T.);
#17804=ORIENTED_EDGE('',*,*,#12481,.F.);
#17805=ORIENTED_EDGE('',*,*,#12407,.F.);
#17806=ORIENTED_EDGE('',*,*,#12479,.F.);
#17807=ORIENTED_EDGE('',*,*,#12450,.T.);
#17808=ORIENTED_EDGE('',*,*,#12440,.T.);
#17809=ORIENTED_EDGE('',*,*,#12408,.T.);
#17810=ORIENTED_EDGE('',*,*,#12481,.T.);
#17811=ORIENTED_EDGE('',*,*,#12482,.F.);
#17812=ORIENTED_EDGE('',*,*,#12445,.F.);
#17813=ORIENTED_EDGE('',*,*,#12478,.F.);
#17814=ORIENTED_EDGE('',*,*,#12483,.T.);
#17815=ORIENTED_EDGE('',*,*,#12470,.T.);
#17816=ORIENTED_EDGE('',*,*,#12423,.F.);
#17817=ORIENTED_EDGE('',*,*,#12435,.F.);
#17818=ORIENTED_EDGE('',*,*,#12469,.F.);
#17819=ORIENTED_EDGE('',*,*,#12441,.T.);
#17820=ORIENTED_EDGE('',*,*,#12482,.T.);
#17821=ORIENTED_EDGE('',*,*,#12480,.F.);
#17822=ORIENTED_EDGE('',*,*,#12327,.T.);
#17823=ORIENTED_EDGE('',*,*,#12324,.T.);
#17824=ORIENTED_EDGE('',*,*,#12321,.T.);
#17825=ORIENTED_EDGE('',*,*,#12330,.T.);
#17826=ORIENTED_EDGE('',*,*,#12339,.T.);
#17827=ORIENTED_EDGE('',*,*,#12336,.T.);
#17828=ORIENTED_EDGE('',*,*,#12333,.T.);
#17829=ORIENTED_EDGE('',*,*,#12342,.T.);
#17830=ORIENTED_EDGE('',*,*,#12351,.T.);
#17831=ORIENTED_EDGE('',*,*,#12348,.T.);
#17832=ORIENTED_EDGE('',*,*,#12345,.T.);
#17833=ORIENTED_EDGE('',*,*,#12354,.T.);
#17834=ORIENTED_EDGE('',*,*,#12363,.T.);
#17835=ORIENTED_EDGE('',*,*,#12360,.T.);
#17836=ORIENTED_EDGE('',*,*,#12357,.T.);
#17837=ORIENTED_EDGE('',*,*,#12366,.T.);
#17838=ORIENTED_EDGE('',*,*,#12375,.T.);
#17839=ORIENTED_EDGE('',*,*,#12372,.T.);
#17840=ORIENTED_EDGE('',*,*,#12369,.T.);
#17841=ORIENTED_EDGE('',*,*,#12378,.T.);
#17842=ORIENTED_EDGE('',*,*,#12387,.T.);
#17843=ORIENTED_EDGE('',*,*,#12384,.T.);
#17844=ORIENTED_EDGE('',*,*,#12381,.T.);
#17845=ORIENTED_EDGE('',*,*,#12390,.T.);
#17846=ORIENTED_EDGE('',*,*,#12484,.T.);
#17847=ORIENTED_EDGE('',*,*,#12471,.T.);
#17848=ORIENTED_EDGE('',*,*,#12483,.F.);
#17849=ORIENTED_EDGE('',*,*,#12477,.F.);
#17850=ORIENTED_EDGE('',*,*,#12474,.T.);
#17851=ORIENTED_EDGE('',*,*,#12472,.T.);
#17852=ORIENTED_EDGE('',*,*,#12484,.F.);
#17853=ORIENTED_EDGE('',*,*,#12476,.F.);
#19379=ADVANCED_FACE('',(#5663),#979,.F.);
#19380=ADVANCED_FACE('',(#5664),#980,.F.);
#19381=ADVANCED_FACE('',(#5665),#981,.F.);
#19382=ADVANCED_FACE('',(#5666),#982,.F.);
#19383=ADVANCED_FACE('',(#5667),#983,.F.);
#19384=ADVANCED_FACE('',(#5668),#984,.F.);
#19385=ADVANCED_FACE('',(#5669),#985,.F.);
#19386=ADVANCED_FACE('',(#5670),#986,.F.);
#19387=ADVANCED_FACE('',(#5671),#987,.F.);
#19388=ADVANCED_FACE('',(#5672),#988,.F.);
#19389=ADVANCED_FACE('',(#5673),#989,.F.);
#19390=ADVANCED_FACE('',(#5674),#990,.F.);
#19391=ADVANCED_FACE('',(#5675),#991,.F.);
#19392=ADVANCED_FACE('',(#5676),#992,.F.);
#19393=ADVANCED_FACE('',(#5677),#993,.F.);
#19394=ADVANCED_FACE('',(#5678),#994,.F.);
#19395=ADVANCED_FACE('',(#5679),#995,.F.);
#19396=ADVANCED_FACE('',(#5680),#996,.F.);
#19397=ADVANCED_FACE('',(#5681),#997,.F.);
#19398=ADVANCED_FACE('',(#5682),#998,.F.);
#19399=ADVANCED_FACE('',(#5683),#999,.F.);
#19400=ADVANCED_FACE('',(#5684),#1000,.F.);
#19401=ADVANCED_FACE('',(#5685),#1001,.F.);
#19402=ADVANCED_FACE('',(#5686),#1002,.F.);
#19403=ADVANCED_FACE('',(#5687),#1003,.F.);
#19404=ADVANCED_FACE('',(#5688),#1004,.F.);
#19405=ADVANCED_FACE('',(#5689),#1005,.F.);
#19406=ADVANCED_FACE('',(#5690),#1006,.T.);
#19407=ADVANCED_FACE('',(#5691),#1007,.F.);
#19408=ADVANCED_FACE('',(#5692),#1008,.F.);
#19409=ADVANCED_FACE('',(#5693,#572,#573,#574,#575,#576,#577),#1009,.F.);
#19410=ADVANCED_FACE('',(#5694),#1010,.F.);
#19411=ADVANCED_FACE('',(#5695),#1011,.F.);
#19412=ADVANCED_FACE('',(#5696),#1012,.F.);
#19413=ADVANCED_FACE('',(#5697),#1013,.F.);
#19414=ADVANCED_FACE('',(#5698),#1014,.F.);
#19415=ADVANCED_FACE('',(#5699),#1015,.F.);
#19416=ADVANCED_FACE('',(#5700),#1016,.F.);
#19417=ADVANCED_FACE('',(#5701),#1017,.F.);
#19418=ADVANCED_FACE('',(#5702),#1018,.F.);
#19419=ADVANCED_FACE('',(#5703),#1019,.T.);
#19420=ADVANCED_FACE('',(#5704),#1020,.F.);
#19421=ADVANCED_FACE('',(#5705),#1021,.F.);
#19422=ADVANCED_FACE('',(#5706),#1022,.F.);
#19423=ADVANCED_FACE('',(#5707),#1023,.F.);
#19424=ADVANCED_FACE('',(#5708),#1024,.F.);
#19425=ADVANCED_FACE('',(#5709),#1025,.T.);
#19426=ADVANCED_FACE('',(#5710),#1026,.F.);
#19427=ADVANCED_FACE('',(#5711),#1027,.F.);
#19428=ADVANCED_FACE('',(#5712),#1028,.F.);
#19429=ADVANCED_FACE('',(#5713),#1029,.F.);
#19430=ADVANCED_FACE('',(#5714,#578,#579,#580,#581,#582,#583),#1030,.F.);
#19431=ADVANCED_FACE('',(#5715),#1031,.F.);
#19432=ADVANCED_FACE('',(#5716),#1032,.F.);
#19580=CLOSED_SHELL('',(#19379,#19380,#19381,#19382,#19383,#19384,#19385,
#19386,#19387,#19388,#19389,#19390,#19391,#19392,#19393,#19394,#19395,#19396,
#19397,#19398,#19399,#19400,#19401,#19402,#19403,#19404,#19405,#19406,#19407,
#19408,#19409,#19410,#19411,#19412,#19413,#19414,#19415,#19416,#19417,#19418,
#19419,#19420,#19421,#19422,#19423,#19424,#19425,#19426,#19427,#19428,#19429,
#19430,#19431,#19432));
#21904=AXIS2_PLACEMENT_3D('',#33586,#27444,#27445);
#21905=AXIS2_PLACEMENT_3D('',#33587,#27446,#27447);
#21906=AXIS2_PLACEMENT_3D('',#33596,#27452,#27453);
#21907=AXIS2_PLACEMENT_3D('',#33602,#27457,#27458);
#21908=AXIS2_PLACEMENT_3D('',#33608,#27462,#27463);
#21909=AXIS2_PLACEMENT_3D('',#33611,#27466,#27467);
#21910=AXIS2_PLACEMENT_3D('',#33620,#27472,#27473);
#21911=AXIS2_PLACEMENT_3D('',#33626,#27477,#27478);
#21912=AXIS2_PLACEMENT_3D('',#33632,#27482,#27483);
#21913=AXIS2_PLACEMENT_3D('',#33635,#27486,#27487);
#21914=AXIS2_PLACEMENT_3D('',#33644,#27492,#27493);
#21915=AXIS2_PLACEMENT_3D('',#33650,#27497,#27498);
#21916=AXIS2_PLACEMENT_3D('',#33656,#27502,#27503);
#21917=AXIS2_PLACEMENT_3D('',#33659,#27506,#27507);
#21918=AXIS2_PLACEMENT_3D('',#33668,#27512,#27513);
#21919=AXIS2_PLACEMENT_3D('',#33674,#27517,#27518);
#21920=AXIS2_PLACEMENT_3D('',#33680,#27522,#27523);
#21921=AXIS2_PLACEMENT_3D('',#33683,#27526,#27527);
#21922=AXIS2_PLACEMENT_3D('',#33692,#27532,#27533);
#21923=AXIS2_PLACEMENT_3D('',#33698,#27537,#27538);
#21924=AXIS2_PLACEMENT_3D('',#33704,#27542,#27543);
#21925=AXIS2_PLACEMENT_3D('',#33707,#27546,#27547);
#21926=AXIS2_PLACEMENT_3D('',#33716,#27552,#27553);
#21927=AXIS2_PLACEMENT_3D('',#33722,#27557,#27558);
#21928=AXIS2_PLACEMENT_3D('',#33728,#27562,#27563);
#21929=AXIS2_PLACEMENT_3D('',#33731,#27566,#27567);
#21930=AXIS2_PLACEMENT_3D('',#33740,#27572,#27573);
#21931=AXIS2_PLACEMENT_3D('',#33746,#27577,#27578);
#21932=AXIS2_PLACEMENT_3D('',#33752,#27582,#27583);
#21933=AXIS2_PLACEMENT_3D('',#33762,#27589,#27590);
#21934=AXIS2_PLACEMENT_3D('',#33770,#27595,#27596);
#21935=AXIS2_PLACEMENT_3D('',#33776,#27600,#27601);
#21936=AXIS2_PLACEMENT_3D('',#33796,#27612,#27613);
#21937=AXIS2_PLACEMENT_3D('',#33802,#27617,#27618);
#21938=AXIS2_PLACEMENT_3D('',#33811,#27623,#27624);
#21939=AXIS2_PLACEMENT_3D('',#33814,#27627,#27628);
#21940=AXIS2_PLACEMENT_3D('',#33822,#27633,#27634);
#21941=AXIS2_PLACEMENT_3D('',#33838,#27644,#27645);
#21942=AXIS2_PLACEMENT_3D('',#33844,#27649,#27650);
#21943=AXIS2_PLACEMENT_3D('',#33850,#27654,#27655);
#21944=AXIS2_PLACEMENT_3D('',#33852,#27657,#27658);
#21945=AXIS2_PLACEMENT_3D('',#33861,#27663,#27664);
#21946=AXIS2_PLACEMENT_3D('',#33867,#27668,#27669);
#21947=AXIS2_PLACEMENT_3D('',#33873,#27673,#27674);
#21948=AXIS2_PLACEMENT_3D('',#33880,#27679,#27680);
#21949=AXIS2_PLACEMENT_3D('',#33884,#27684,#27685);
#21950=AXIS2_PLACEMENT_3D('',#33885,#27686,#27687);
#21951=AXIS2_PLACEMENT_3D('',#33887,#27689,#27690);
#21952=AXIS2_PLACEMENT_3D('',#33895,#27695,#27696);
#21953=AXIS2_PLACEMENT_3D('',#33899,#27699,#27700);
#21954=AXIS2_PLACEMENT_3D('',#33906,#27705,#27706);
#21955=AXIS2_PLACEMENT_3D('',#33910,#27709,#27710);
#21956=AXIS2_PLACEMENT_3D('',#33912,#27712,#27713);
#21957=AXIS2_PLACEMENT_3D('',#33914,#27715,#27716);
#21958=AXIS2_PLACEMENT_3D('',#33916,#27718,#27719);
#27444=DIRECTION('axis',(0.,0.,1.));
#27445=DIRECTION('refdir',(1.,0.,0.));
#27446=DIRECTION('center_axis',(-5.6420062889325E-16,1.,6.61092274672818E-17));
#27447=DIRECTION('ref_axis',(-9.50035731417012E-15,6.61092274672764E-17,
-1.));
#27448=DIRECTION('',(-1.00001914094641E-12,-1.00108821931263E-12,1.));
#27449=DIRECTION('',(-1.,9.99435799370104E-13,-1.0001463424449E-12));
#27450=DIRECTION('',(9.99999999998985E-13,1.00108821931263E-12,-1.));
#27451=DIRECTION('',(-1.,9.99435799370104E-13,-1.0001463424449E-12));
#27452=DIRECTION('center_axis',(-1.46342445914483E-16,-4.41888838750563E-15,
1.));
#27453=DIRECTION('ref_axis',(1.,3.89820370584558E-15,1.463424459145E-16));
#27454=DIRECTION('',(-9.99485797221669E-13,-1.,-1.00441888838649E-12));
#27455=DIRECTION('',(9.99479153109799E-13,1.,1.00441888838649E-12));
#27456=DIRECTION('',(-1.,9.99435799370104E-13,-1.0001463424449E-12));
#27457=DIRECTION('center_axis',(5.64200628893241E-16,-1.,2.20037109950003E-17));
#27458=DIRECTION('ref_axis',(-1.,-5.64200628893241E-16,1.0522467400333E-14));
#27459=DIRECTION('',(1.00001914094642E-12,-1.00002200370999E-12,-1.));
#27460=DIRECTION('',(-9.99999999998993E-13,1.00002200370999E-12,1.));
#27461=DIRECTION('',(-1.,9.99435799370104E-13,-1.0001463424449E-12));
#27462=DIRECTION('center_axis',(-1.0522467400333E-14,4.4188883875057E-15,
-1.));
#27463=DIRECTION('ref_axis',(1.,-6.77060614040192E-15,-1.0522467400333E-14));
#27464=DIRECTION('',(9.99485797221669E-13,1.,1.00441888838649E-12));
#27465=DIRECTION('',(-9.99479153109799E-13,-1.,-1.00441888838649E-12));
#27466=DIRECTION('center_axis',(-2.79702568992599E-16,2.20037109950002E-17,
1.));
#27467=DIRECTION('ref_axis',(1.,3.89820370584558E-15,2.79702568992599E-16));
#27468=DIRECTION('',(-9.99485797221648E-13,-1.,1.00002200371E-12));
#27469=DIRECTION('',(-1.,9.99435799370104E-13,-1.00027970256798E-12));
#27470=DIRECTION('',(9.99479153109778E-13,1.,-1.00002200371E-12));
#27471=DIRECTION('',(-1.,9.99435799370104E-13,-1.00027970256798E-12));
#27472=DIRECTION('center_axis',(5.64200628893241E-16,-1.,2.20037109950003E-17));
#27473=DIRECTION('ref_axis',(-1.,-5.64200628893241E-16,1.0522467400333E-14));
#27474=DIRECTION('',(1.00001914094642E-12,-1.00002200370999E-12,-1.));
#27475=DIRECTION('',(-9.99999999998993E-13,1.00002200370999E-12,1.));
#27476=DIRECTION('',(-1.,9.99435799370104E-13,-1.00027970256798E-12));
#27477=DIRECTION('center_axis',(-1.0522467400333E-14,-2.20037109949256E-17,
-1.));
#27478=DIRECTION('ref_axis',(1.,-6.90396626348002E-15,-1.0522467400333E-14));
#27479=DIRECTION('',(9.99485797221648E-13,1.,-1.00002200371E-12));
#27480=DIRECTION('',(-9.99479153109778E-13,-1.,1.00002200371E-12));
#27481=DIRECTION('',(-1.,9.99435799370104E-13,-1.00027970256798E-12));
#27482=DIRECTION('center_axis',(-5.6420062889324E-16,1.,6.61092274672781E-17));
#27483=DIRECTION('ref_axis',(-1.06105803387953E-14,6.61092274672721E-17,
-1.));
#27484=DIRECTION('',(-1.00001914094642E-12,1.00002200370999E-12,1.));
#27485=DIRECTION('',(9.99999999998993E-13,-1.00002200370999E-12,-1.));
#27486=DIRECTION('center_axis',(-1.0522467400333E-14,-2.2003710994928E-17,
-1.));
#27487=DIRECTION('ref_axis',(1.,-6.77060614040192E-15,-1.0522467400333E-14));
#27488=DIRECTION('',(9.99485797221648E-13,1.,-1.00002200371E-12));
#27489=DIRECTION('',(-1.,9.99435799370104E-13,-1.0001463424449E-12));
#27490=DIRECTION('',(-9.99479153109778E-13,-1.,1.00002200371E-12));
#27491=DIRECTION('',(-1.,9.99435799370104E-13,-1.0001463424449E-12));
#27492=DIRECTION('center_axis',(-5.6420062889324E-16,1.,6.61092274672781E-17));
#27493=DIRECTION('ref_axis',(-1.06105803387953E-14,6.61092274672721E-17,
-1.));
#27494=DIRECTION('',(-1.00001914094642E-12,1.00002200370999E-12,1.));
#27495=DIRECTION('',(9.99999999998993E-13,-1.00002200370999E-12,-1.));
#27496=DIRECTION('',(-1.,9.99435799370104E-13,-1.0001463424449E-12));
#27497=DIRECTION('center_axis',(-1.46342445914518E-16,4.46289580949563E-15,
1.));
#27498=DIRECTION('ref_axis',(1.,3.89820370584558E-15,1.46342445914501E-16));
#27499=DIRECTION('',(-9.9948579722165E-13,-1.,1.0044628958085E-12));
#27500=DIRECTION('',(9.99479153109778E-13,1.,-1.0044628958085E-12));
#27501=DIRECTION('',(-1.,9.99435799370104E-13,-1.0001463424449E-12));
#27502=DIRECTION('center_axis',(5.64200628893241E-16,-1.,2.20037109950003E-17));
#27503=DIRECTION('ref_axis',(-1.,-5.64200628893241E-16,1.0522467400333E-14));
#27504=DIRECTION('',(1.00001914094642E-12,-1.00002200370999E-12,-1.));
#27505=DIRECTION('',(-9.99999999998993E-13,1.00002200370999E-12,1.));
#27506=DIRECTION('center_axis',(-5.6420062889325E-16,1.,6.61092274672818E-17));
#27507=DIRECTION('ref_axis',(-9.50035731417012E-15,6.61092274672764E-17,
-1.));
#27508=DIRECTION('',(-1.00001914094641E-12,-1.00108821931263E-12,1.));
#27509=DIRECTION('',(-1.,9.99435799370104E-13,-1.0001463424449E-12));
#27510=DIRECTION('',(9.99999999998985E-13,1.00108821931263E-12,-1.));
#27511=DIRECTION('',(-1.,9.99435799370104E-13,-1.0001463424449E-12));
#27512=DIRECTION('center_axis',(-1.46342445914518E-16,4.46289580949563E-15,
1.));
#27513=DIRECTION('ref_axis',(1.,3.89820370584558E-15,1.46342445914501E-16));
#27514=DIRECTION('',(-9.9948579722165E-13,-1.,1.0044628958085E-12));
#27515=DIRECTION('',(9.99479153109778E-13,1.,-1.0044628958085E-12));
#27516=DIRECTION('',(-1.,9.99435799370104E-13,-1.0001463424449E-12));
#27517=DIRECTION('center_axis',(5.64200628893241E-16,-1.,2.20037109950003E-17));
#27518=DIRECTION('ref_axis',(-1.,-5.64200628893241E-16,1.0522467400333E-14));
#27519=DIRECTION('',(1.00001914094642E-12,-1.00002200370999E-12,-1.));
#27520=DIRECTION('',(-9.99999999998993E-13,1.00002200370999E-12,1.));
#27521=DIRECTION('',(-1.,9.99435799370104E-13,-1.0001463424449E-12));
#27522=DIRECTION('center_axis',(-1.0522467400333E-14,-4.46289580949556E-15,
-1.));
#27523=DIRECTION('ref_axis',(1.,-6.77060614040192E-15,-1.0522467400333E-14));
#27524=DIRECTION('',(9.9948579722165E-13,1.,-1.0044628958085E-12));
#27525=DIRECTION('',(-9.99479153109778E-13,-1.,1.0044628958085E-12));
#27526=DIRECTION('center_axis',(5.64200628893243E-16,-1.,1.13222673562016E-15));
#27527=DIRECTION('ref_axis',(-1.,-5.64200628893231E-16,1.0522467400333E-14));
#27528=DIRECTION('',(1.00001914094642E-12,-1.00113222673461E-12,-1.));
#27529=DIRECTION('',(-1.,9.99435799370104E-13,-1.00027970256798E-12));
#27530=DIRECTION('',(-9.99999999998993E-13,1.00113222673461E-12,1.));
#27531=DIRECTION('',(-1.,9.99435799370104E-13,-1.00027970256798E-12));
#27532=DIRECTION('center_axis',(-1.0522467400333E-14,2.19844233825538E-15,
-1.));
#27533=DIRECTION('ref_axis',(1.,-6.90396626348002E-15,-1.0522467400333E-14));
#27534=DIRECTION('',(9.99485797221669E-13,1.,1.00219844233724E-12));
#27535=DIRECTION('',(-9.99479153109799E-13,-1.,-1.00219844233724E-12));
#27536=DIRECTION('',(-1.,9.99435799370104E-13,-1.00027970256798E-12));
#27537=DIRECTION('center_axis',(-5.6420062889324E-16,1.,6.61092274672781E-17));
#27538=DIRECTION('ref_axis',(-1.06105803387953E-14,6.61092274672721E-17,
-1.));
#27539=DIRECTION('',(-1.00001914094642E-12,1.00002200370999E-12,1.));
#27540=DIRECTION('',(9.99999999998993E-13,-1.00002200370999E-12,-1.));
#27541=DIRECTION('',(-1.,9.99435799370104E-13,-1.00027970256798E-12));
#27542=DIRECTION('center_axis',(-2.79702568992582E-16,-4.41888838750562E-15,
1.));
#27543=DIRECTION('ref_axis',(1.,3.89820370584558E-15,2.79702568992599E-16));
#27544=DIRECTION('',(-9.99485797221669E-13,-1.,-1.00441888838649E-12));
#27545=DIRECTION('',(9.99479153109799E-13,1.,1.00441888838649E-12));
#27546=DIRECTION('center_axis',(5.64200628893241E-16,-1.,2.20037109950003E-17));
#27547=DIRECTION('ref_axis',(-1.,-5.64200628893241E-16,1.0522467400333E-14));
#27548=DIRECTION('',(1.00001914094642E-12,-1.00002200370999E-12,-1.));
#27549=DIRECTION('',(-1.,9.99435799370104E-13,-1.0001463424449E-12));
#27550=DIRECTION('',(-9.99999999998993E-13,1.00002200370999E-12,1.));
#27551=DIRECTION('',(-1.,9.99435799370104E-13,-1.0001463424449E-12));
#27552=DIRECTION('center_axis',(-1.0522467400333E-14,-2.2003710994928E-17,
-1.));
#27553=DIRECTION('ref_axis',(1.,-6.77060614040192E-15,-1.0522467400333E-14));
#27554=DIRECTION('',(9.99485797221648E-13,1.,-1.00002200371E-12));
#27555=DIRECTION('',(-9.99479153109778E-13,-1.,1.00002200371E-12));
#27556=DIRECTION('',(-1.,9.99435799370104E-13,-1.0001463424449E-12));
#27557=DIRECTION('center_axis',(-5.6420062889324E-16,1.,6.61092274672781E-17));
#27558=DIRECTION('ref_axis',(-1.06105803387953E-14,6.61092274672721E-17,
-1.));
#27559=DIRECTION('',(-1.00001914094642E-12,1.00002200370999E-12,1.));
#27560=DIRECTION('',(9.99999999998993E-13,-1.00002200370999E-12,-1.));
#27561=DIRECTION('',(-1.,9.99435799370104E-13,-1.0001463424449E-12));
#27562=DIRECTION('center_axis',(-1.46342445914501E-16,2.20037109950002E-17,
1.));
#27563=DIRECTION('ref_axis',(1.,3.89820370584558E-15,1.46342445914501E-16));
#27564=DIRECTION('',(-9.99485797221648E-13,-1.,1.00002200371E-12));
#27565=DIRECTION('',(9.99479153109778E-13,1.,-1.00002200371E-12));
#27566=DIRECTION('center_axis',(-1.,-3.89820370584558E-15,2.74254865331501E-16));
#27567=DIRECTION('ref_axis',(3.89820370584558E-15,-1.,-6.61092274673135E-17));
#27568=DIRECTION('',(-9.99725745133657E-13,-6.61092274712107E-17,1.));
#27569=DIRECTION('',(-9.96101796293144E-13,-1.,9.99999999999011E-13));
#27570=DIRECTION('',(-9.99725745133657E-13,-6.61092274712107E-17,1.));
#27571=DIRECTION('',(9.96101796293144E-13,1.,-9.99999999999011E-13));
#27572=DIRECTION('center_axis',(-3.89820370584558E-15,1.,6.61092274673135E-17));
#27573=DIRECTION('ref_axis',(-1.0522467400333E-14,6.61092274672725E-17,
-1.));
#27574=DIRECTION('',(-1.,-3.89820370584552E-15,-9.99999999998989E-13));
#27575=DIRECTION('',(9.99999999998989E-13,6.61092274712117E-17,-1.));
#27576=DIRECTION('',(1.,3.89820370584552E-15,9.99999999998989E-13));
#27577=DIRECTION('center_axis',(3.89820370584558E-15,-1.,-6.61092274673135E-17));
#27578=DIRECTION('ref_axis',(-1.,-3.89820370584558E-15,1.0522467400333E-14));
#27579=DIRECTION('',(1.,3.89820370584552E-15,9.99999999998989E-13));
#27580=DIRECTION('',(-1.,-3.89820370584552E-15,-9.99999999998989E-13));
#27581=DIRECTION('',(-9.99999999998989E-13,-6.61092274712117E-17,1.));
#27582=DIRECTION('center_axis',(0.,3.71824206197546E-31,1.));
#27583=DIRECTION('ref_axis',(1.,3.89820370584558E-15,-1.44944649852236E-45));
#27584=DIRECTION('',(-9.60161374617363E-15,-1.,1.E-14));
#27585=DIRECTION('',(1.,-9.60161374617374E-15,9.9999999999998E-15));
#27586=DIRECTION('',(9.47915311079142E-15,1.,-1.E-14));
#27587=DIRECTION('',(1.,-9.99693694313996E-13,9.99999999998989E-13));
#27588=DIRECTION('',(-9.60161374617363E-15,-1.,1.E-14));
#27589=DIRECTION('center_axis',(-1.,-3.98386253826119E-16,0.));
#27590=DIRECTION('ref_axis',(3.98386253826119E-16,-1.,-6.61092274672767E-17));
#27591=DIRECTION('',(-9.60161374617363E-15,-1.,1.E-14));
#27592=DIRECTION('',(9.99999999999984E-15,-9.99999999999985E-15,-1.));
#27593=DIRECTION('',(-9.60670630755441E-15,-1.,1.E-14));
#27594=DIRECTION('',(-9.99999999999984E-15,9.99999999999985E-15,1.));
#27595=DIRECTION('center_axis',(-3.0630568499948E-16,1.,6.61092274672757E-17));
#27596=DIRECTION('ref_axis',(-1.0522467400333E-14,6.61092274672725E-17,
-1.));
#27597=DIRECTION('',(-1.00001914094642E-12,9.99933890771529E-13,1.));
#27598=DIRECTION('',(-1.,9.99693694313996E-13,-9.99999999998989E-13));
#27599=DIRECTION('',(9.99999999998993E-13,-9.99933890771529E-13,-1.));
#27600=DIRECTION('center_axis',(1.,5.1420277733694E-16,-1.0522467400333E-14));
#27601=DIRECTION('ref_axis',(-1.0522467400333E-14,1.06077175752244E-14,
-1.));
#27602=DIRECTION('',(-9.99999999999984E-15,9.99999999999985E-15,1.));
#27603=DIRECTION('',(-9.99485797221669E-13,-1.,-1.0001493759533E-12));
#27604=DIRECTION('',(1.00001914094641E-12,1.00006610922647E-12,-1.));
#27605=DIRECTION('',(9.99485797221669E-13,1.,1.00006610922646E-12));
#27606=DIRECTION('',(-9.99999999999984E-15,9.99999999999985E-15,1.));
#27607=DIRECTION('',(-9.99485797221669E-13,-1.,-1.00006610922646E-12));
#27608=DIRECTION('',(1.00001914094642E-12,-9.99933890771529E-13,-1.));
#27609=DIRECTION('',(9.99485797221669E-13,1.,1.0001493759533E-12));
#27610=DIRECTION('',(-9.99999999999984E-15,9.99999999999985E-15,1.));
#27611=DIRECTION('',(9.47915311079142E-15,1.,-1.E-14));
#27612=DIRECTION('center_axis',(3.36838938541509E-16,-1.,-6.61092274673116E-17));
#27613=DIRECTION('ref_axis',(-1.,-3.3683893854151E-16,1.0522467400333E-14));
#27614=DIRECTION('',(9.99999999999984E-15,-9.99999999999985E-15,-1.));
#27615=DIRECTION('',(-1.,9.99645538472762E-13,-9.99999999998989E-13));
#27616=DIRECTION('',(1.,-9.99663161060454E-13,9.99999999998989E-13));
#27617=DIRECTION('center_axis',(1.,-3.83971434457208E-15,-1.05224674003331E-14));
#27618=DIRECTION('ref_axis',(-1.05224674003331E-14,1.00581164490937E-14,
-1.));
#27619=DIRECTION('',(-1.00383971434355E-12,-1.,9.99999999999011E-13));
#27620=DIRECTION('',(9.99469539820287E-13,-9.99999999998997E-13,-1.));
#27621=DIRECTION('',(1.00383971434355E-12,1.,-9.99999999999011E-13));
#27622=DIRECTION('',(-9.99469539820287E-13,9.99999999998997E-13,1.));
#27623=DIRECTION('center_axis',(5.30460178706591E-16,-6.61092274673115E-17,
1.));
#27624=DIRECTION('ref_axis',(1.,3.89820370584558E-15,-5.30460178706591E-16));
#27625=DIRECTION('',(-1.,9.9960161374517E-13,-9.99469539820283E-13));
#27626=DIRECTION('',(1.,-9.9960670630655E-13,9.99469539820283E-13));
#27627=DIRECTION('center_axis',(-3.9329369244535E-16,1.,6.61092274672764E-17));
#27628=DIRECTION('ref_axis',(-1.05885766278003E-14,6.61092274672722E-17,
-1.));
#27629=DIRECTION('',(1.,-9.60670630755452E-15,9.9999999999998E-15));
#27630=DIRECTION('',(9.99999999999984E-15,-9.99999999999985E-15,-1.));
#27631=DIRECTION('',(1.,-9.60670630755452E-15,1.01020425574102E-14));
#27632=DIRECTION('',(9.99999999999984E-15,-9.99999999999985E-15,-1.));
#27633=DIRECTION('center_axis',(3.98386253826121E-16,-1.,1.20031049926069E-31));
#27634=DIRECTION('ref_axis',(-1.,-3.98386253826121E-16,1.0522467400333E-14));
#27635=DIRECTION('',(1.,-9.9960161374517E-13,9.99999999998989E-13));
#27636=DIRECTION('',(1.,-9.9960161374517E-13,1.00057976284491E-12));
#27637=DIRECTION('',(-1.00057976284491E-12,9.99999999998997E-13,1.));
#27638=DIRECTION('',(-1.,9.9960161374517E-13,-9.99999999998989E-13));
#27639=DIRECTION('',(1.,-9.60161374617374E-15,1.0306127672231E-14));
#27640=DIRECTION('',(-1.01141265444719E-14,9.99999999999985E-15,1.));
#27641=DIRECTION('',(-1.,9.60161374617374E-15,-1.01020425574102E-14));
#27642=DIRECTION('',(-9.99999999999984E-15,9.99999999999985E-15,1.));
#27643=DIRECTION('',(1.,-9.60161374617374E-15,9.9999999999998E-15));
#27644=DIRECTION('center_axis',(4.794216935078E-16,-1.,-6.61092274673155E-17));
#27645=DIRECTION('ref_axis',(-1.,-4.79421693507801E-16,1.0522467400333E-14));
#27646=DIRECTION('',(9.99999999999984E-15,-9.99999999999985E-15,-1.));
#27647=DIRECTION('',(-1.,9.99520578305488E-13,-9.99999999998989E-13));
#27648=DIRECTION('',(-1.,9.99520578305488E-13,-9.99999999998989E-13));
#27649=DIRECTION('center_axis',(1.,-2.9746054942148E-15,-1.05224674003331E-14));
#27650=DIRECTION('ref_axis',(-1.05224674003331E-14,1.11683394737189E-14,
-1.));
#27651=DIRECTION('',(-1.0029746054932E-12,-1.,9.99999999999011E-13));
#27652=DIRECTION('',(-1.0029746054932E-12,-1.,9.99999999999011E-13));
#27653=DIRECTION('',(1.00057976284491E-12,-9.99999999998997E-13,-1.));
#27654=DIRECTION('center_axis',(-1.0522467400333E-14,6.61092274673958E-17,
-1.));
#27655=DIRECTION('ref_axis',(1.,-7.20402654040602E-15,-1.0522467400333E-14));
#27656=DIRECTION('',(-1.,9.9960670630655E-13,-1.00057976284491E-12));
#27657=DIRECTION('center_axis',(-1.,-3.89820370584558E-15,2.74254865331601E-16));
#27658=DIRECTION('ref_axis',(3.89820370584558E-15,-1.,-6.61092274673135E-17));
#27659=DIRECTION('',(-9.99725745133657E-13,-6.61092274712107E-17,1.));
#27660=DIRECTION('',(9.96101796293144E-13,1.,-9.99999999999011E-13));
#27661=DIRECTION('',(9.99725745133657E-13,6.61092274712107E-17,-1.));
#27662=DIRECTION('',(-9.96101796293144E-13,-1.,9.99999999999011E-13));
#27663=DIRECTION('center_axis',(3.89820370584558E-15,-1.,-6.61092274673135E-17));
#27664=DIRECTION('ref_axis',(-1.,-3.89820370584558E-15,1.0522467400333E-14));
#27665=DIRECTION('',(-1.,-3.89820370584552E-15,-9.99999999998989E-13));
#27666=DIRECTION('',(9.99999999998989E-13,6.61092274712117E-17,-1.));
#27667=DIRECTION('',(1.,3.89820370584552E-15,9.99999999998989E-13));
#27668=DIRECTION('center_axis',(3.89820370584558E-15,-1.,-6.61092274673135E-17));
#27669=DIRECTION('ref_axis',(-1.,-3.89820370584558E-15,1.0522467400333E-14));
#27670=DIRECTION('',(1.,3.89820370584552E-15,9.99999999998989E-13));
#27671=DIRECTION('',(-1.,-3.89820370584552E-15,-9.99999999998989E-13));
#27672=DIRECTION('',(-9.99999999998989E-13,-6.61092274712117E-17,1.));
#27673=DIRECTION('center_axis',(-1.,-3.98386253826119E-16,0.));
#27674=DIRECTION('ref_axis',(3.98386253826119E-16,-1.,-6.61092274672767E-17));
#27675=DIRECTION('',(-9.60161374617363E-15,-1.,1.E-14));
#27676=DIRECTION('',(-9.60161374617363E-15,-1.,1.E-14));
#27677=DIRECTION('',(9.99999999999984E-15,-9.99999999999985E-15,-1.));
#27678=DIRECTION('',(-9.60161374617363E-15,-1.,1.E-14));
#27679=DIRECTION('center_axis',(-1.,-3.98386253826119E-16,0.));
#27680=DIRECTION('ref_axis',(3.98386253826119E-16,-1.,-6.61092274672767E-17));
#27681=DIRECTION('',(-9.60161374617363E-15,-1.,1.E-14));
#27682=DIRECTION('',(-9.60670630755441E-15,-1.,1.E-14));
#27683=DIRECTION('',(-9.60161374617363E-15,-1.,1.E-14));
#27684=DIRECTION('center_axis',(0.,3.71824206197546E-31,1.));
#27685=DIRECTION('ref_axis',(1.,3.89820370584558E-15,-1.44944649852236E-45));
#27686=DIRECTION('center_axis',(-1.0522467400333E-14,7.23040323441634E-29,
-1.));
#27687=DIRECTION('ref_axis',(1.,-6.72630625189782E-15,-1.0522467400333E-14));
#27688=DIRECTION('',(-9.60670630755441E-15,-1.,1.E-14));
#27689=DIRECTION('center_axis',(0.,3.71824206197546E-31,1.));
#27690=DIRECTION('ref_axis',(1.,3.89820370584558E-15,-1.44944649852236E-45));
#27691=DIRECTION('',(9.47915311079142E-15,1.,-1.E-14));
#27692=DIRECTION('',(0.707106781186548,0.707106781186547,9.99999999999976E-15));
#27693=DIRECTION('',(9.47915311079142E-15,1.,-1.E-14));
#27694=DIRECTION('',(-1.,9.65799058254168E-15,-9.9999999999998E-15));
#27695=DIRECTION('center_axis',(3.42009417458172E-16,-1.,7.1325447274173E-31));
#27696=DIRECTION('ref_axis',(-1.,-3.42009417458172E-16,1.0522467400333E-14));
#27697=DIRECTION('',(9.99999999999984E-15,-9.99999999999985E-15,-1.));
#27698=DIRECTION('',(-1.,9.65799058254168E-15,-9.9999999999998E-15));
#27699=DIRECTION('center_axis',(0.,3.71824206197546E-31,1.));
#27700=DIRECTION('ref_axis',(1.,3.89820370584558E-15,-1.44944649852236E-45));
#27701=DIRECTION('',(9.47915311079142E-15,1.,-1.E-14));
#27702=DIRECTION('',(0.707106781186548,0.707106781186547,9.99999999999976E-15));
#27703=DIRECTION('',(9.47915311079142E-15,1.,-1.E-14));
#27704=DIRECTION('',(1.,-9.60670630755452E-15,9.9999999999998E-15));
#27705=DIRECTION('center_axis',(-3.9329369244535E-16,1.,6.61092274672764E-17));
#27706=DIRECTION('ref_axis',(-1.05885766278003E-14,6.61092274672722E-17,
-1.));
#27707=DIRECTION('',(9.99999999999984E-15,-9.99999999999985E-15,-1.));
#27708=DIRECTION('',(-1.,9.60670630755452E-15,-1.0306127672231E-14));
#27709=DIRECTION('center_axis',(-3.06127672231199E-16,-2.03369632909008E-32,
1.));
#27710=DIRECTION('ref_axis',(1.,3.89820370584558E-15,3.06127672231199E-16));
#27711=DIRECTION('',(-9.60670630755441E-15,-1.,1.E-14));
#27712=DIRECTION('center_axis',(-1.,-5.20846889208359E-16,0.));
#27713=DIRECTION('ref_axis',(5.20846889208359E-16,-1.,-6.6109227467278E-17));
#27714=DIRECTION('',(9.99999999999984E-15,-9.99999999999985E-15,-1.));
#27715=DIRECTION('center_axis',(-0.707106781186547,0.707106781186548,1.10440526730942E-29));
#27716=DIRECTION('ref_axis',(-6.61092274672986E-17,-6.61092274673141E-17,
1.));
#27717=DIRECTION('',(9.99999999999984E-15,-9.99999999999985E-15,-1.));
#27718=DIRECTION('center_axis',(-1.,-5.20846889208359E-16,0.));
#27719=DIRECTION('ref_axis',(5.20846889208359E-16,-1.,-6.6109227467278E-17));
#33586=CARTESIAN_POINT('',(0.,0.,0.));
#33587=CARTESIAN_POINT('Origin',(0.0262,-0.02495,0.00124999999999987));
#33588=CARTESIAN_POINT('',(0.02115,-0.02495,0.000749999999999928));
#33589=CARTESIAN_POINT('',(0.02115,-0.02495,0.00124999999999993));
#33590=CARTESIAN_POINT('',(0.02115000000001,-0.02495000000001,-0.00524999999999003));
#33591=CARTESIAN_POINT('',(0.0229,-0.02495,0.000749999999999909));
#33592=CARTESIAN_POINT('',(0.0262000000000101,-0.02495000000001,0.000750000000009974));
#33593=CARTESIAN_POINT('',(0.0229,-0.02495,0.00124999999999991));
#33594=CARTESIAN_POINT('',(0.0229000000000101,-0.02495000000001,0.00377500000000991));
#33595=CARTESIAN_POINT('',(0.0262000000000101,-0.02495000000001,0.00125000000000997));
#33596=CARTESIAN_POINT('Origin',(0.0262,-0.02545,0.00124999999999987));
#33597=CARTESIAN_POINT('',(0.02115,-0.02545,0.00124999999999993));
#33598=CARTESIAN_POINT('',(0.0211500000000101,-0.02387500000001,0.00125000000000993));
#33599=CARTESIAN_POINT('',(0.0229,-0.02545,0.00124999999999991));
#33600=CARTESIAN_POINT('',(0.0229000000000101,-0.0247750000000099,0.00125000000000991));
#33601=CARTESIAN_POINT('',(0.0262000000000101,-0.02545000000001,0.00125000000000997));
#33602=CARTESIAN_POINT('Origin',(0.0262,-0.02545,0.000749999999999874));
#33603=CARTESIAN_POINT('',(0.02115,-0.02545,0.000749999999999928));
#33604=CARTESIAN_POINT('',(0.02115000000001,-0.02545000000001,-0.00549999999999003));
#33605=CARTESIAN_POINT('',(0.0229,-0.02545,0.000749999999999909));
#33606=CARTESIAN_POINT('',(0.0229000000000101,-0.02545000000001,0.00352500000000991));
#33607=CARTESIAN_POINT('',(0.0262000000000101,-0.02545000000001,0.000750000000009974));
#33608=CARTESIAN_POINT('Origin',(0.0262,-0.02495,0.000749999999999874));
#33609=CARTESIAN_POINT('',(0.0211500000000101,-0.02362500000001,0.000750000000009929));
#33610=CARTESIAN_POINT('',(0.0229000000000101,-0.02452500000001,0.000750000000009909));
#33611=CARTESIAN_POINT('Origin',(0.0262,-0.02545,-0.00475000000000013));
#33612=CARTESIAN_POINT('',(0.02115,-0.02495,-0.00475000000000007));
#33613=CARTESIAN_POINT('',(0.02115,-0.02545,-0.00475000000000007));
#33614=CARTESIAN_POINT('',(0.02115000000001,-0.02387500000001,-0.00474999999999007));
#33615=CARTESIAN_POINT('',(0.0229,-0.02495,-0.00475000000000009));
#33616=CARTESIAN_POINT('',(0.0262000000000101,-0.02495000000001,-0.00474999999999007));
#33617=CARTESIAN_POINT('',(0.0229,-0.02545,-0.00475000000000009));
#33618=CARTESIAN_POINT('',(0.0229000000000101,-0.02477500000001,-0.00474999999999007));
#33619=CARTESIAN_POINT('',(0.0262000000000101,-0.02545000000001,-0.00474999999999007));
#33620=CARTESIAN_POINT('Origin',(0.0262,-0.02545,-0.00525000000000013));
#33621=CARTESIAN_POINT('',(0.02115,-0.02545,-0.00525000000000007));
#33622=CARTESIAN_POINT('',(0.0211500000000101,-0.02545000000001,-0.00849999999999003));
#33623=CARTESIAN_POINT('',(0.0229,-0.02545,-0.00525000000000009));
#33624=CARTESIAN_POINT('',(0.0229000000000101,-0.02545000000001,0.000525000000009908));
#33625=CARTESIAN_POINT('',(0.0262000000000101,-0.02545000000001,-0.00524999999999008));
#33626=CARTESIAN_POINT('Origin',(0.0262,-0.02495,-0.00525000000000013));
#33627=CARTESIAN_POINT('',(0.02115,-0.02495,-0.00525000000000007));
#33628=CARTESIAN_POINT('',(0.0211500000000101,-0.02362500000001,-0.00524999999999007));
#33629=CARTESIAN_POINT('',(0.0229,-0.02495,-0.00525000000000009));
#33630=CARTESIAN_POINT('',(0.0229000000000101,-0.02452500000001,-0.00524999999999007));
#33631=CARTESIAN_POINT('',(0.0262000000000101,-0.02495000000001,-0.00524999999999008));
#33632=CARTESIAN_POINT('Origin',(0.0262,-0.02495,-0.00475000000000013));
#33633=CARTESIAN_POINT('',(0.0211500000000101,-0.02495000000001,-0.00824999999999003));
#33634=CARTESIAN_POINT('',(0.0229000000000101,-0.02495000000001,0.000775000000009908));
#33635=CARTESIAN_POINT('Origin',(0.0262,-0.02495,0.00274999999999987));
#33636=CARTESIAN_POINT('',(0.02115,-0.02545,0.00274999999999993));
#33637=CARTESIAN_POINT('',(0.02115,-0.02495,0.00274999999999993));
#33638=CARTESIAN_POINT('',(0.02115000000001,-0.02362500000001,0.00275000000000993));
#33639=CARTESIAN_POINT('',(0.0229,-0.02545,0.00274999999999991));
#33640=CARTESIAN_POINT('',(0.0262000000000101,-0.02545000000001,0.00275000000000997));
#33641=CARTESIAN_POINT('',(0.0229,-0.02495,0.00274999999999991));
#33642=CARTESIAN_POINT('',(0.0229000000000101,-0.02452500000001,0.00275000000000991));
#33643=CARTESIAN_POINT('',(0.0262000000000101,-0.02495000000001,0.00275000000000997));
#33644=CARTESIAN_POINT('Origin',(0.0262,-0.02495,0.00324999999999987));
#33645=CARTESIAN_POINT('',(0.02115,-0.02495,0.00324999999999992));
#33646=CARTESIAN_POINT('',(0.02115000000001,-0.02495000000001,-0.00424999999999004));
#33647=CARTESIAN_POINT('',(0.0229,-0.02495,0.00324999999999991));
#33648=CARTESIAN_POINT('',(0.0229000000000101,-0.02495000000001,0.00477500000000991));
#33649=CARTESIAN_POINT('',(0.0262000000000101,-0.02495000000001,0.00325000000000997));
#33650=CARTESIAN_POINT('Origin',(0.0262,-0.02545,0.00324999999999987));
#33651=CARTESIAN_POINT('',(0.02115,-0.02545,0.00324999999999992));
#33652=CARTESIAN_POINT('',(0.0211500000000101,-0.02387500000001,0.00325000000000992));
#33653=CARTESIAN_POINT('',(0.0229,-0.02545,0.00324999999999991));
#33654=CARTESIAN_POINT('',(0.0229000000000101,-0.02477500000001,0.00325000000000991));
#33655=CARTESIAN_POINT('',(0.0262000000000101,-0.02545000000001,0.00325000000000997));
#33656=CARTESIAN_POINT('Origin',(0.0262,-0.02545,0.00274999999999987));
#33657=CARTESIAN_POINT('',(0.0211500000000101,-0.02545000000001,-0.00449999999999003));
#33658=CARTESIAN_POINT('',(0.0229000000000101,-0.02545000000001,0.00452500000000991));
#33659=CARTESIAN_POINT('Origin',(0.0262,-0.02495,-0.000750000000000127));
#33660=CARTESIAN_POINT('',(0.02115,-0.02495,-0.00125000000000007));
#33661=CARTESIAN_POINT('',(0.02115,-0.02495,-0.000750000000000074));
#33662=CARTESIAN_POINT('',(0.02115000000001,-0.02495000000001,-0.00624999999999003));
#33663=CARTESIAN_POINT('',(0.0229,-0.02495,-0.00125000000000009));
#33664=CARTESIAN_POINT('',(0.0262000000000102,-0.02495000000001,-0.00124999999999003));
#33665=CARTESIAN_POINT('',(0.0229,-0.02495,-0.000750000000000093));
#33666=CARTESIAN_POINT('',(0.0229000000000101,-0.02495000000001,0.00277500000000991));
#33667=CARTESIAN_POINT('',(0.0262000000000101,-0.02495000000001,-0.000749999999990028));
#33668=CARTESIAN_POINT('Origin',(0.0262,-0.02545,-0.000750000000000127));
#33669=CARTESIAN_POINT('',(0.02115,-0.02545,-0.000750000000000074));
#33670=CARTESIAN_POINT('',(0.0211500000000101,-0.02387500000001,-0.000749999999990073));
#33671=CARTESIAN_POINT('',(0.0229,-0.02545,-0.000750000000000093));
#33672=CARTESIAN_POINT('',(0.0229000000000101,-0.02477500000001,-0.000749999999990092));
#33673=CARTESIAN_POINT('',(0.0262000000000101,-0.02545000000001,-0.000749999999990028));
#33674=CARTESIAN_POINT('Origin',(0.0262,-0.02545,-0.00125000000000013));
#33675=CARTESIAN_POINT('',(0.02115,-0.02545,-0.00125000000000007));
#33676=CARTESIAN_POINT('',(0.02115000000001,-0.02545000000001,-0.00649999999999003));
#33677=CARTESIAN_POINT('',(0.0229,-0.02545,-0.00125000000000009));
#33678=CARTESIAN_POINT('',(0.0229000000000101,-0.02545000000001,0.00252500000000991));
#33679=CARTESIAN_POINT('',(0.0262000000000102,-0.02545000000001,-0.00124999999999003));
#33680=CARTESIAN_POINT('Origin',(0.0262,-0.02495,-0.00125000000000013));
#33681=CARTESIAN_POINT('',(0.0211500000000101,-0.02362500000001,-0.00124999999999007));
#33682=CARTESIAN_POINT('',(0.0229000000000101,-0.02452500000001,-0.00124999999999009));
#33683=CARTESIAN_POINT('Origin',(0.0262,-0.02545,-0.00325000000000012));
#33684=CARTESIAN_POINT('',(0.02115,-0.02545,-0.00275000000000007));
#33685=CARTESIAN_POINT('',(0.02115,-0.02545,-0.00325000000000007));
#33686=CARTESIAN_POINT('',(0.0211500000000101,-0.02545000000001,-0.00749999999999003));
#33687=CARTESIAN_POINT('',(0.0229,-0.02545,-0.00275000000000009));
#33688=CARTESIAN_POINT('',(0.0262000000000101,-0.02545000000001,-0.00274999999999008));
#33689=CARTESIAN_POINT('',(0.0229,-0.02545,-0.00325000000000009));
#33690=CARTESIAN_POINT('',(0.0229000000000101,-0.02545000000001,0.00152500000000991));
#33691=CARTESIAN_POINT('',(0.0262000000000101,-0.02545000000001,-0.00324999999999008));
#33692=CARTESIAN_POINT('Origin',(0.0262,-0.02495,-0.00325000000000012));
#33693=CARTESIAN_POINT('',(0.02115,-0.02495,-0.00325000000000007));
#33694=CARTESIAN_POINT('',(0.0211500000000101,-0.02362500000001,-0.00324999999999007));
#33695=CARTESIAN_POINT('',(0.0229,-0.02495,-0.00325000000000009));
#33696=CARTESIAN_POINT('',(0.0229000000000101,-0.02452500000001,-0.00324999999999007));
#33697=CARTESIAN_POINT('',(0.0262000000000101,-0.02495000000001,-0.00324999999999008));
#33698=CARTESIAN_POINT('Origin',(0.0262,-0.02495,-0.00275000000000013));
#33699=CARTESIAN_POINT('',(0.02115,-0.02495,-0.00275000000000007));
#33700=CARTESIAN_POINT('',(0.0211500000000101,-0.02495000000001,-0.00724999999999003));
#33701=CARTESIAN_POINT('',(0.0229,-0.02495,-0.00275000000000009));
#33702=CARTESIAN_POINT('',(0.0229000000000101,-0.02495000000001,0.00177500000000991));
#33703=CARTESIAN_POINT('',(0.0262000000000101,-0.02495000000001,-0.00274999999999007));
#33704=CARTESIAN_POINT('Origin',(0.0262,-0.02545,-0.00275000000000013));
#33705=CARTESIAN_POINT('',(0.02115000000001,-0.02387500000001,-0.00274999999999007));
#33706=CARTESIAN_POINT('',(0.0229000000000101,-0.0247750000000099,-0.00274999999999008));
#33707=CARTESIAN_POINT('Origin',(0.0262,-0.02545,0.00474999999999988));
#33708=CARTESIAN_POINT('',(0.02115,-0.02545,0.00524999999999993));
#33709=CARTESIAN_POINT('',(0.02115,-0.02545,0.00474999999999993));
#33710=CARTESIAN_POINT('',(0.02115000000001,-0.02545000000001,-0.00349999999999003));
#33711=CARTESIAN_POINT('',(0.0229,-0.02545,0.00524999999999991));
#33712=CARTESIAN_POINT('',(0.0262000000000101,-0.02545000000001,0.00525000000000998));
#33713=CARTESIAN_POINT('',(0.0229,-0.02545,0.00474999999999991));
#33714=CARTESIAN_POINT('',(0.0229000000000101,-0.02545000000001,0.00552500000000991));
#33715=CARTESIAN_POINT('',(0.0262000000000101,-0.02545000000001,0.00475000000000998));
#33716=CARTESIAN_POINT('Origin',(0.0262,-0.02495,0.00474999999999988));
#33717=CARTESIAN_POINT('',(0.02115,-0.02495,0.00474999999999993));
#33718=CARTESIAN_POINT('',(0.02115000000001,-0.02362500000001,0.00475000000000993));
#33719=CARTESIAN_POINT('',(0.0229,-0.02495,0.00474999999999991));
#33720=CARTESIAN_POINT('',(0.0229000000000101,-0.02452500000001,0.00475000000000991));
#33721=CARTESIAN_POINT('',(0.0262000000000101,-0.02495000000001,0.00475000000000998));
#33722=CARTESIAN_POINT('Origin',(0.0262,-0.02495,0.00524999999999988));
#33723=CARTESIAN_POINT('',(0.02115,-0.02495,0.00524999999999993));
#33724=CARTESIAN_POINT('',(0.02115000000001,-0.02495000000001,-0.00324999999999003));
#33725=CARTESIAN_POINT('',(0.0229,-0.02495,0.00524999999999991));
#33726=CARTESIAN_POINT('',(0.0229000000000101,-0.02495000000001,0.00577500000000991));
#33727=CARTESIAN_POINT('',(0.0262000000000101,-0.02495000000001,0.00525000000000998));
#33728=CARTESIAN_POINT('Origin',(0.0262,-0.02545,0.00524999999999988));
#33729=CARTESIAN_POINT('',(0.0211500000000101,-0.02387500000001,0.00525000000000993));
#33730=CARTESIAN_POINT('',(0.0229000000000101,-0.02477500000001,0.00525000000000991));
#33731=CARTESIAN_POINT('Origin',(0.02525,-0.02575,0.00629999999999988));
#33732=CARTESIAN_POINT('',(0.02525,-0.02575,0.00629999999999988));
#33733=CARTESIAN_POINT('',(0.02525,-0.02575,0.00694999999999988));
#33734=CARTESIAN_POINT('',(0.0252500000000101,-0.0257500000000099,0.00630000000000988));
#33735=CARTESIAN_POINT('',(0.02525,-0.02495,0.00629999999999988));
#33736=CARTESIAN_POINT('',(0.0252500000000101,-0.0249250000000099,0.00630000000000988));
#33737=CARTESIAN_POINT('',(0.02525,-0.02495,0.00694999999999988));
#33738=CARTESIAN_POINT('',(0.0252500000000101,-0.02495000000001,0.00630000000000988));
#33739=CARTESIAN_POINT('',(0.0252500000000101,-0.02462500000001,0.00695000000000988));
#33740=CARTESIAN_POINT('Origin',(0.0262,-0.02495,0.00662499999999987));
#33741=CARTESIAN_POINT('',(0.02715,-0.02495,0.00629999999999987));
#33742=CARTESIAN_POINT('',(0.0266750000000101,-0.02495000000001,0.00630000000000997));
#33743=CARTESIAN_POINT('',(0.02715,-0.02495,0.00694999999999987));
#33744=CARTESIAN_POINT('',(0.0271500000000101,-0.02495000000001,-0.000162499999990037));
#33745=CARTESIAN_POINT('',(0.0266750000000101,-0.02495000000001,0.00695000000000997));
#33746=CARTESIAN_POINT('Origin',(0.0262,-0.02575,0.00662499999999987));
#33747=CARTESIAN_POINT('',(0.02715,-0.02575,0.00629999999999987));
#33748=CARTESIAN_POINT('',(0.0266750000000101,-0.0257500000000099,0.00630000000000997));
#33749=CARTESIAN_POINT('',(0.02715,-0.02575,0.00694999999999987));
#33750=CARTESIAN_POINT('',(0.0266750000000101,-0.0257500000000099,0.00695000000000997));
#33751=CARTESIAN_POINT('',(0.0271500000000101,-0.0257500000000099,-0.000162499999990037));
#33752=CARTESIAN_POINT('Origin',(0.02715,-0.0235,0.00694999999999987));
#33753=CARTESIAN_POINT('',(0.02715,-0.0235,0.00694999999999987));
#33754=CARTESIAN_POINT('',(0.0271500000000101,-0.02350000000001,0.00695000000000997));
#33755=CARTESIAN_POINT('',(0.02115,-0.0235,0.00695));
#33756=CARTESIAN_POINT('',(0.0271500000000101,-0.02350000000001,0.00695000000000997));
#33757=CARTESIAN_POINT('',(0.02115,-0.0283,0.00695));
#33758=CARTESIAN_POINT('',(0.02115000000001,-0.02350000000001,0.00695000000000993));
#33759=CARTESIAN_POINT('',(0.02715,-0.0283,0.00694999999999987));
#33760=CARTESIAN_POINT('',(0.0253521645021746,-0.02830000000001,0.00695000000000988));
#33761=CARTESIAN_POINT('',(0.0271500000000101,-0.02350000000001,0.00695000000000997));
#33762=CARTESIAN_POINT('Origin',(0.02715,-0.0235,-0.00695000000000008));
#33763=CARTESIAN_POINT('',(0.02715,-0.0241,0.00629999999999987));
#33764=CARTESIAN_POINT('',(0.0271500000000101,-0.02410000000001,0.00630000000000996));
#33765=CARTESIAN_POINT('',(0.02715,-0.0241,0.00379999999999987));
#33766=CARTESIAN_POINT('',(0.0271500000000101,-0.02410000000001,0.00630000000000996));
#33767=CARTESIAN_POINT('',(0.02715,-0.0235,0.00379999999999987));
#33768=CARTESIAN_POINT('',(0.0271500000000101,-0.0234990000000099,0.00380000000000996));
#33769=CARTESIAN_POINT('',(0.0271500000000101,-0.02350000000001,-0.00694999999999008));
#33770=CARTESIAN_POINT('Origin',(0.0235543290043291,-0.0283,-9.8879238130678E-17));
#33771=CARTESIAN_POINT('',(0.02115,-0.0283,-0.00695));
#33772=CARTESIAN_POINT('',(0.0211500000000101,-0.02830000000001,-0.00587499999999003));
#33773=CARTESIAN_POINT('',(0.02715,-0.0283,-0.00695000000000008));
#33774=CARTESIAN_POINT('',(0.0253521645021746,-0.02830000000001,-0.00694999999999008));
#33775=CARTESIAN_POINT('',(0.0271500000000101,-0.0283000000000099,-0.00347499999999008));
#33776=CARTESIAN_POINT('Origin',(0.02115,-0.0223,-0.01175));
#33777=CARTESIAN_POINT('',(0.02115,-0.0235,0.00629999999999993));
#33778=CARTESIAN_POINT('',(0.0211500000000101,-0.02350000000001,-0.00694999999999007));
#33779=CARTESIAN_POINT('',(0.02115,-0.0241,0.00629999999999993));
#33780=CARTESIAN_POINT('',(0.0211500000000101,-0.02305000000001,0.00630000000000993));
#33781=CARTESIAN_POINT('',(0.02115,-0.0241,0.00529999999999993));
#33782=CARTESIAN_POINT('',(0.0211500000000101,-0.02410000000001,-0.00272499999999003));
#33783=CARTESIAN_POINT('',(0.02115,-0.0235,0.00529999999999993));
#33784=CARTESIAN_POINT('',(0.02115000000001,-0.02305000000001,0.00530000000000993));
#33785=CARTESIAN_POINT('',(0.02115,-0.0235,-0.00530000000000007));
#33786=CARTESIAN_POINT('',(0.0211500000000101,-0.02350000000001,-0.00694999999999007));
#33787=CARTESIAN_POINT('',(0.02115,-0.0241,-0.00530000000000007));
#33788=CARTESIAN_POINT('',(0.02115000000001,-0.02305000000001,-0.00529999999999007));
#33789=CARTESIAN_POINT('',(0.02115,-0.0241,-0.00630000000000007));
#33790=CARTESIAN_POINT('',(0.0211500000000101,-0.02410000000001,-0.00902499999999003));
#33791=CARTESIAN_POINT('',(0.02115,-0.0235,-0.00630000000000007));
#33792=CARTESIAN_POINT('',(0.02115000000001,-0.02305000000001,-0.00629999999999007));
#33793=CARTESIAN_POINT('',(0.02115,-0.0235,-0.00695));
#33794=CARTESIAN_POINT('',(0.0211500000000101,-0.02350000000001,-0.00694999999999007));
#33795=CARTESIAN_POINT('',(0.0211500000000101,-0.02350000000001,-0.00694999999999007));
#33796=CARTESIAN_POINT('Origin',(0.02115,-0.0241,-0.00630000000000007));
#33797=CARTESIAN_POINT('',(0.0229,-0.0241,-0.00530000000000009));
#33798=CARTESIAN_POINT('',(0.0229,-0.0241,-0.00630000000000009));
#33799=CARTESIAN_POINT('',(0.0229000000000101,-0.02410000000001,0.00630000000000991));
#33800=CARTESIAN_POINT('',(0.02515000000001,-0.02410000000001,-0.00629999999999008));
#33801=CARTESIAN_POINT('',(0.0229000000000101,-0.02410000000001,-0.00529999999999007));
#33802=CARTESIAN_POINT('Origin',(0.02515,-0.0241,-0.00630000000000012));
#33803=CARTESIAN_POINT('',(0.02515,-0.0235,-0.00630000000000012));
#33804=CARTESIAN_POINT('',(0.02515,-0.0241,-0.00630000000000012));
#33805=CARTESIAN_POINT('',(0.02515000000001,-0.02350000000001,-0.00629999999999008));
#33806=CARTESIAN_POINT('',(0.02515,-0.0241,-0.00530000000000012));
#33807=CARTESIAN_POINT('',(0.02515000000001,-0.02410000000001,9.88618908959182E-15));
#33808=CARTESIAN_POINT('',(0.02515,-0.0235,-0.00530000000000012));
#33809=CARTESIAN_POINT('',(0.0251500000000101,-0.02350000000001,-0.00529999999999008));
#33810=CARTESIAN_POINT('',(0.02515000000001,-0.02350000000001,-0.00662499999999008));
#33811=CARTESIAN_POINT('Origin',(0.02315,-0.0238,-0.0053000000000001));
#33812=CARTESIAN_POINT('',(0.0251500000000101,-0.02350000000001,-0.00529999999999008));
#33813=CARTESIAN_POINT('',(0.0251500000000101,-0.02410000000001,-0.00529999999999008));
#33814=CARTESIAN_POINT('Origin',(0.02715,-0.0241,0.00629999999999987));
#33815=CARTESIAN_POINT('',(0.02715,-0.0241,-0.00630000000000008));
#33816=CARTESIAN_POINT('',(0.0271500000000101,-0.02410000000001,-0.00629999999999008));
#33817=CARTESIAN_POINT('',(0.02715,-0.0241,-0.00380000000000013));
#33818=CARTESIAN_POINT('',(0.0271500000000101,-0.02410000000001,0.00630000000000996));
#33819=CARTESIAN_POINT('',(0.0229,-0.0241,-0.00380000000000009));
#33820=CARTESIAN_POINT('',(0.0271500000000101,-0.02410000000001,-0.00379999999999007));
#33821=CARTESIAN_POINT('',(0.0229000000000101,-0.02410000000001,0.00630000000000991));
#33822=CARTESIAN_POINT('Origin',(0.02715,-0.0235,-0.00695000000000008));
#33823=CARTESIAN_POINT('',(0.02515000000001,-0.02350000000001,-0.00629999999999008));
#33824=CARTESIAN_POINT('',(0.02515,-0.0235,0.00529999999999989));
#33825=CARTESIAN_POINT('',(0.0251500000000101,-0.02350000000001,0.00530000000000988));
#33826=CARTESIAN_POINT('',(0.02515,-0.0235,0.00629999999999989));
#33827=CARTESIAN_POINT('',(0.0251500000000102,-0.02350000000001,-0.000324999999990115));
#33828=CARTESIAN_POINT('',(0.0251500000000101,-0.02350000000001,0.00630000000000988));
#33829=CARTESIAN_POINT('',(0.0229,-0.0235,0.00379999999999991));
#33830=CARTESIAN_POINT('',(0.0271500000000101,-0.02350000000001,0.00380000000000996));
#33831=CARTESIAN_POINT('',(0.0229,-0.0235,-0.00380000000000009));
#33832=CARTESIAN_POINT('',(0.0229000000000101,-0.02350000000001,-0.00379999999999007));
#33833=CARTESIAN_POINT('',(0.02715,-0.0235,-0.00380000000000013));
#33834=CARTESIAN_POINT('',(0.0271500000000101,-0.02350000000001,-0.00379999999999008));
#33835=CARTESIAN_POINT('',(0.02715,-0.0235,-0.00695000000000008));
#33836=CARTESIAN_POINT('',(0.0271500000000101,-0.02350000000001,-0.00694999999999008));
#33837=CARTESIAN_POINT('',(0.0271500000000101,-0.02350000000001,-0.00694999999999008));
#33838=CARTESIAN_POINT('Origin',(0.02515,-0.0241,0.00629999999999989));
#33839=CARTESIAN_POINT('',(0.0229,-0.0241,0.00629999999999991));
#33840=CARTESIAN_POINT('',(0.0229,-0.0241,0.00529999999999991));
#33841=CARTESIAN_POINT('',(0.0229000000000101,-0.02410000000001,0.00630000000000991));
#33842=CARTESIAN_POINT('',(0.0251500000000101,-0.02410000000001,0.00530000000000988));
#33843=CARTESIAN_POINT('',(0.0251500000000101,-0.02410000000001,0.00630000000000988));
#33844=CARTESIAN_POINT('Origin',(0.02515,-0.0235,0.00629999999999989));
#33845=CARTESIAN_POINT('',(0.02515,-0.0241,0.00629999999999989));
#33846=CARTESIAN_POINT('',(0.0251500000000101,-0.02350000000001,0.00630000000000988));
#33847=CARTESIAN_POINT('',(0.02515,-0.0241,0.00529999999999989));
#33848=CARTESIAN_POINT('',(0.0251500000000101,-0.02350000000001,0.00530000000000988));
#33849=CARTESIAN_POINT('',(0.0251500000000101,-0.02410000000001,0.00630000000000988));
#33850=CARTESIAN_POINT('Origin',(0.02315,-0.0238,0.00529999999999991));
#33851=CARTESIAN_POINT('',(0.0251500000000101,-0.02410000000001,0.00530000000000988));
#33852=CARTESIAN_POINT('Origin',(0.02525,-0.02495,-0.00630000000000012));
#33853=CARTESIAN_POINT('',(0.02525,-0.02495,-0.00695000000000012));
#33854=CARTESIAN_POINT('',(0.02525,-0.02495,-0.00630000000000012));
#33855=CARTESIAN_POINT('',(0.0252500000000101,-0.02495000000001,-0.00694999999999008));
#33856=CARTESIAN_POINT('',(0.02525,-0.02575,-0.00630000000000012));
#33857=CARTESIAN_POINT('',(0.0252500000000101,-0.02452500000001,-0.00629999999999008));
#33858=CARTESIAN_POINT('',(0.02525,-0.02575,-0.00695000000000012));
#33859=CARTESIAN_POINT('',(0.0252500000000101,-0.0257500000000099,-0.00694999999999008));
#33860=CARTESIAN_POINT('',(0.0252500000000101,-0.02422500000001,-0.00694999999999008));
#33861=CARTESIAN_POINT('Origin',(0.0262,-0.02495,-0.00662500000000013));
#33862=CARTESIAN_POINT('',(0.02715,-0.02495,-0.00695000000000008));
#33863=CARTESIAN_POINT('',(0.0266750000000101,-0.02495000000001,-0.00694999999999007));
#33864=CARTESIAN_POINT('',(0.02715,-0.02495,-0.00630000000000008));
#33865=CARTESIAN_POINT('',(0.0271500000000101,-0.02495000000001,-0.00678749999999008));
#33866=CARTESIAN_POINT('',(0.0266750000000101,-0.02495000000001,-0.00629999999999007));
#33867=CARTESIAN_POINT('Origin',(0.0262,-0.02575,-0.00662500000000013));
#33868=CARTESIAN_POINT('',(0.02715,-0.02575,-0.00695000000000008));
#33869=CARTESIAN_POINT('',(0.0266750000000101,-0.0257500000000099,-0.00694999999999007));
#33870=CARTESIAN_POINT('',(0.02715,-0.02575,-0.00630000000000008));
#33871=CARTESIAN_POINT('',(0.0266750000000101,-0.0257500000000099,-0.00629999999999007));
#33872=CARTESIAN_POINT('',(0.0271500000000101,-0.0257500000000099,-0.00678749999999008));
#33873=CARTESIAN_POINT('Origin',(0.02715,-0.0235,-0.00695000000000008));
#33874=CARTESIAN_POINT('',(0.0271500000000101,-0.02350000000001,-0.00694999999999008));
#33875=CARTESIAN_POINT('',(0.02715,-0.0276,-0.00630000000000008));
#33876=CARTESIAN_POINT('',(0.0271500000000101,-0.02410000000001,-0.00629999999999008));
#33877=CARTESIAN_POINT('',(0.02715,-0.0276,0.00629999999999987));
#33878=CARTESIAN_POINT('',(0.0271500000000101,-0.0276000000000099,0.00630000000000996));
#33879=CARTESIAN_POINT('',(0.0271500000000101,-0.02410000000001,0.00630000000000996));
#33880=CARTESIAN_POINT('Origin',(0.02715,-0.0235,-0.00695000000000008));
#33881=CARTESIAN_POINT('',(0.0271500000000101,-0.02350000000001,-0.00694999999999008));
#33882=CARTESIAN_POINT('',(0.0271500000000101,-0.0234990000000099,-0.00379999999999008));
#33883=CARTESIAN_POINT('',(0.0271500000000101,-0.02410000000001,-0.00629999999999008));
#33884=CARTESIAN_POINT('Origin',(0.02715,-0.0235,-0.00695000000000008));
#33885=CARTESIAN_POINT('Origin',(0.02715,-0.023499,-0.00380000000000013));
#33886=CARTESIAN_POINT('',(0.0229000000000101,-0.02349900000001,-0.00379999999999007));
#33887=CARTESIAN_POINT('Origin',(0.02715,-0.0241,-0.00630000000000008));
#33888=CARTESIAN_POINT('',(0.0229,-0.02575,-0.00630000000000009));
#33889=CARTESIAN_POINT('',(0.0229000000000101,-0.02410000000001,-0.00629999999999007));
#33890=CARTESIAN_POINT('',(0.0223,-0.02635,-0.00630000000000009));
#33891=CARTESIAN_POINT('',(0.0229000000000101,-0.02575000000001,-0.00629999999999007));
#33892=CARTESIAN_POINT('',(0.0223,-0.0276,-0.00630000000000009));
#33893=CARTESIAN_POINT('',(0.0223000000000101,-0.0263500000000099,-0.00629999999999008));
#33894=CARTESIAN_POINT('',(0.0271500000000101,-0.0276000000000099,-0.00629999999999008));
#33895=CARTESIAN_POINT('Origin',(0.02715,-0.0276,0.00629999999999987));
#33896=CARTESIAN_POINT('',(0.0223,-0.0276,0.00629999999999991));
#33897=CARTESIAN_POINT('',(0.0223000000000101,-0.0276000000000099,0.00630000000000991));
#33898=CARTESIAN_POINT('',(0.0271500000000101,-0.0276000000000099,0.00630000000000996));
#33899=CARTESIAN_POINT('Origin',(0.02715,-0.0241,0.00629999999999987));
#33900=CARTESIAN_POINT('',(0.0223,-0.02635,0.00629999999999991));
#33901=CARTESIAN_POINT('',(0.0223000000000101,-0.0263500000000099,0.00630000000000991));
#33902=CARTESIAN_POINT('',(0.0229,-0.02575,0.00629999999999991));
#33903=CARTESIAN_POINT('',(0.0229000000000101,-0.02575000000001,0.00630000000000991));
#33904=CARTESIAN_POINT('',(0.0229000000000101,-0.02410000000001,0.00630000000000991));
#33905=CARTESIAN_POINT('',(0.0271500000000101,-0.02410000000001,0.00630000000000996));
#33906=CARTESIAN_POINT('Origin',(0.02715,-0.0241,0.00629999999999987));
#33907=CARTESIAN_POINT('',(0.0229,-0.0241,0.00379999999999991));
#33908=CARTESIAN_POINT('',(0.0229000000000101,-0.02410000000001,0.00630000000000991));
#33909=CARTESIAN_POINT('',(0.0271500000000101,-0.02410000000001,0.00380000000000996));
#33910=CARTESIAN_POINT('Origin',(0.02715,-0.023499,0.00379999999999987));
#33911=CARTESIAN_POINT('',(0.0229000000000101,-0.02349900000001,0.00380000000000991));
#33912=CARTESIAN_POINT('Origin',(0.0229,-0.0241,0.00629999999999991));
#33913=CARTESIAN_POINT('',(0.0229000000000101,-0.02575000000001,0.00630000000000991));
#33914=CARTESIAN_POINT('Origin',(0.0229,-0.02575,0.00629999999999991));
#33915=CARTESIAN_POINT('',(0.0223000000000101,-0.0263500000000099,0.00630000000000991));
#33916=CARTESIAN_POINT('Origin',(0.0223,-0.02635,0.00629999999999991));
#34834=UNCERTAINTY_MEASURE_WITH_UNIT(LENGTH_MEASURE(1.E-5),#34877,
'DISTANCE_ACCURACY_VALUE',
'Maximum model space distance between geometric entities at asserted c
onnectivities');
#34841=UNCERTAINTY_MEASURE_WITH_UNIT(LENGTH_MEASURE(1.E-5),#34877,
'DISTANCE_ACCURACY_VALUE',
'Maximum model space distance between geometric entities at asserted c
onnectivities');
#34869=(
GEOMETRIC_REPRESENTATION_CONTEXT(3)
GLOBAL_UNCERTAINTY_ASSIGNED_CONTEXT((#34834))
GLOBAL_UNIT_ASSIGNED_CONTEXT((#34877,#34878,#34879))
REPRESENTATION_CONTEXT('','3D')
);
#34876=(
GEOMETRIC_REPRESENTATION_CONTEXT(3)
GLOBAL_UNCERTAINTY_ASSIGNED_CONTEXT((#34841))
GLOBAL_UNIT_ASSIGNED_CONTEXT((#34877,#34878,#34879))
REPRESENTATION_CONTEXT('','3D')
);
#34877=(
LENGTH_UNIT()
NAMED_UNIT(*)
SI_UNIT($,.METRE.)
);
#34878=(
NAMED_UNIT(*)
PLANE_ANGLE_UNIT()
SI_UNIT($,.RADIAN.)
);
#34879=(
NAMED_UNIT(*)
SI_UNIT($,.STERADIAN.)
SOLID_ANGLE_UNIT()
);
#34907=SHAPE_DEFINITION_REPRESENTATION(#34941,#35011);
#34941=PRODUCT_DEFINITION_SHAPE('',$,#35046);
#35011=SHAPE_REPRESENTATION('',(#21904),#34869);
#35018=PRODUCT_DEFINITION_CONTEXT('part definition',#35122,'design');
#35046=PRODUCT_DEFINITION('Socket Screw 6','Socket Screw 6',#35080,#35018);
#35080=PRODUCT_DEFINITION_FORMATION('',$,#35151);
#35122=APPLICATION_CONTEXT('Managed model based 3d engineering');
#35123=PRODUCT_CONTEXT('part definition',#35122,'mechanical');
#35151=PRODUCT('Socket Screw 6','Socket Screw 6',
'LEGAL AND USAGE DISCLAIMER: this Data/Model is provided \X2\201C\X0\A
S IS\X2\201D\X0\ for informational and representational only. It is a 
geometric approximation and is NOT engineered, certified, or guarantee
d for dimensional accuracy, exact tolerances, or production-level prec
ision. Vendor disclaims all implied warranties including fitness for a
 particular purpose. DO NOT USE FOR DIRECT PHYSICAL MANUFACTURING, AUT
OMATED PRODUCTION, OR SAFETY-CRITICAL SYSTEMS without independent engi
neering verification and resolution of any design discrepancies.',(#35123));
#35161=PRESENTATION_STYLE_ASSIGNMENT((#35170));
#35170=SURFACE_STYLE_USAGE(.BOTH.,#35179);
#35179=SURFACE_SIDE_STYLE('',(#35188));
#35188=SURFACE_STYLE_FILL_AREA(#35197);
#35197=FILL_AREA_STYLE('Aluminum - Anodized Glossy (Blue)',(#35206));
#35206=FILL_AREA_STYLE_COLOUR('Aluminum - Anodized Glossy (Blue)',#35215);
#35215=COLOUR_RGB('Aluminum - Anodized Glossy (Blue)',0.349019607843137,
0.584313725490196,0.854901960784314);
ENDSEC;
END-ISO-10303-21;
